ISO-10303-21;
HEADER;
/* Generated by software containing ST-Developer
 * from STEP Tools, Inc. (www.steptools.com) 
 */

FILE_DESCRIPTION(
/* description */ (''),
/* implementation_level */ '2;1');

FILE_NAME(
/* name */ 'LINEAR GUIDE.step',
/* time_stamp */ '2026-10-19T01:17:59+06:00',
/* author */ (''),
/* organization */ (''),
/* preprocessor_version */ 'ST-DEVELOPER v20.2',
/* originating_system */ 'Autodesk Translation Framework v15.15.0.0',
/* authorisation */ '');

FILE_SCHEMA (('AUTOMOTIVE_DESIGN { 1 0 10303 214 3 1 1 }'));
ENDSEC;

DATA;
#10=MECHANICAL_DESIGN_GEOMETRIC_PRESENTATION_REPRESENTATION('',(#732,#733,#734),#48369);
#614=SHAPE_REPRESENTATION_RELATIONSHIP('SRR','None',#48414,#625);
#625=ADVANCED_BREP_SHAPE_REPRESENTATION('',(#758,#759,#760),#48359);
#643=FACE_BOUND('',#2435,.T.);
#644=FACE_BOUND('',#2436,.T.);
#645=FACE_BOUND('',#2444,.T.);
#646=FACE_BOUND('',#2445,.T.);
#647=FACE_BOUND('',#2454,.T.);
#648=FACE_BOUND('',#2455,.T.);
#649=FACE_BOUND('',#2465,.T.);
#650=FACE_BOUND('',#2466,.T.);
#732=STYLED_ITEM('',(#48531),#758);
#733=STYLED_ITEM('',(#48531),#759);
#734=STYLED_ITEM('',(#48531),#760);
#758=MANIFOLD_SOLID_BREP('Body1',#20111);
#759=MANIFOLD_SOLID_BREP('Body2',#20112);
#760=MANIFOLD_SOLID_BREP('Body3',#20113);
#835=CYLINDRICAL_SURFACE('',#20511,0.45000000000016);
#836=CYLINDRICAL_SURFACE('',#20513,2.46743797397104);
#837=CYLINDRICAL_SURFACE('',#20515,0.724999999999998);
#838=CYLINDRICAL_SURFACE('',#20518,0.59999999999997);
#839=CYLINDRICAL_SURFACE('',#20520,2.36402292474775);
#840=CYLINDRICAL_SURFACE('',#20522,1.39999999999995);
#841=CYLINDRICAL_SURFACE('',#20525,1.04999999999995);
#842=CYLINDRICAL_SURFACE('',#20528,1.04999999999981);
#843=CYLINDRICAL_SURFACE('',#20538,1.04999999999996);
#844=CYLINDRICAL_SURFACE('',#20546,0.450000000000123);
#845=CYLINDRICAL_SURFACE('',#20548,2.46743797397101);
#846=CYLINDRICAL_SURFACE('',#20550,0.72500000000001);
#847=CYLINDRICAL_SURFACE('',#20553,0.599999999999987);
#848=CYLINDRICAL_SURFACE('',#20555,2.3640229247478);
#849=CYLINDRICAL_SURFACE('',#20557,1.39999999999978);
#850=CYLINDRICAL_SURFACE('',#20560,1.05);
#851=CYLINDRICAL_SURFACE('',#20564,0.45000000000016);
#852=CYLINDRICAL_SURFACE('',#20567,2.46743797397104);
#853=CYLINDRICAL_SURFACE('',#20570,0.724999999999998);
#854=CYLINDRICAL_SURFACE('',#20574,0.59999999999997);
#855=CYLINDRICAL_SURFACE('',#20577,2.36402292474775);
#856=CYLINDRICAL_SURFACE('',#20600,2.16656587073651);
#857=CYLINDRICAL_SURFACE('',#20622,2.16656587073651);
#858=CYLINDRICAL_SURFACE('',#20623,3.00000000000001);
#859=CYLINDRICAL_SURFACE('',#20625,3.00000000000001);
#860=CYLINDRICAL_SURFACE('',#20627,3.00000000000001);
#861=CYLINDRICAL_SURFACE('',#20629,3.00000000000001);
#862=CYLINDRICAL_SURFACE('',#20635,1.04999999999981);
#863=CYLINDRICAL_SURFACE('',#20637,1.04999999999995);
#864=CYLINDRICAL_SURFACE('',#20639,1.39999999999995);
#865=CYLINDRICAL_SURFACE('',#20644,1.04999999999996);
#866=CYLINDRICAL_SURFACE('',#20646,1.05);
#867=CYLINDRICAL_SURFACE('',#20648,1.39999999999978);
#868=CYLINDRICAL_SURFACE('',#20649,2.3640229247478);
#869=CYLINDRICAL_SURFACE('',#20650,0.599999999999987);
#870=CYLINDRICAL_SURFACE('',#20652,0.72500000000001);
#871=CYLINDRICAL_SURFACE('',#20653,2.46743797397101);
#872=CYLINDRICAL_SURFACE('',#20654,0.450000000000123);
#873=CYLINDRICAL_SURFACE('',#20657,1.39999999999995);
#874=CYLINDRICAL_SURFACE('',#20661,1.04999999999995);
#875=CYLINDRICAL_SURFACE('',#20665,1.04999999999981);
#876=CYLINDRICAL_SURFACE('',#20678,1.04999999999996);
#877=CYLINDRICAL_SURFACE('',#20696,1.05);
#878=CYLINDRICAL_SURFACE('',#20699,1.39999999999978);
#879=CYLINDRICAL_SURFACE('',#20701,2.3640229247478);
#880=CYLINDRICAL_SURFACE('',#20703,0.599999999999987);
#881=CYLINDRICAL_SURFACE('',#20706,0.72500000000001);
#882=CYLINDRICAL_SURFACE('',#20708,2.46743797397101);
#883=CYLINDRICAL_SURFACE('',#20710,0.450000000000123);
#884=CYLINDRICAL_SURFACE('',#20715,0.45000000000016);
#885=CYLINDRICAL_SURFACE('',#20717,2.46743797397104);
#886=CYLINDRICAL_SURFACE('',#20719,0.724999999999998);
#887=CYLINDRICAL_SURFACE('',#20722,0.59999999999997);
#888=CYLINDRICAL_SURFACE('',#20724,2.36402292474775);
#1333=FACE_OUTER_BOUND('',#2385,.T.);
#1334=FACE_OUTER_BOUND('',#2386,.T.);
#1335=FACE_OUTER_BOUND('',#2387,.T.);
#1336=FACE_OUTER_BOUND('',#2388,.T.);
#1337=FACE_OUTER_BOUND('',#2389,.T.);
#1338=FACE_OUTER_BOUND('',#2390,.T.);
#1339=FACE_OUTER_BOUND('',#2391,.T.);
#1340=FACE_OUTER_BOUND('',#2392,.T.);
#1341=FACE_OUTER_BOUND('',#2393,.T.);
#1342=FACE_OUTER_BOUND('',#2394,.T.);
#1343=FACE_OUTER_BOUND('',#2395,.T.);
#1344=FACE_OUTER_BOUND('',#2396,.T.);
#1345=FACE_OUTER_BOUND('',#2397,.T.);
#1346=FACE_OUTER_BOUND('',#2398,.T.);
#1347=FACE_OUTER_BOUND('',#2399,.T.);
#1348=FACE_OUTER_BOUND('',#2400,.T.);
#1349=FACE_OUTER_BOUND('',#2401,.T.);
#1350=FACE_OUTER_BOUND('',#2402,.T.);
#1351=FACE_OUTER_BOUND('',#2403,.T.);
#1352=FACE_OUTER_BOUND('',#2404,.T.);
#1353=FACE_OUTER_BOUND('',#2405,.T.);
#1354=FACE_OUTER_BOUND('',#2406,.T.);
#1355=FACE_OUTER_BOUND('',#2407,.T.);
#1356=FACE_OUTER_BOUND('',#2408,.T.);
#1357=FACE_OUTER_BOUND('',#2409,.T.);
#1358=FACE_OUTER_BOUND('',#2410,.T.);
#1359=FACE_OUTER_BOUND('',#2411,.T.);
#1360=FACE_OUTER_BOUND('',#2412,.T.);
#1361=FACE_OUTER_BOUND('',#2413,.T.);
#1362=FACE_OUTER_BOUND('',#2414,.T.);
#1363=FACE_OUTER_BOUND('',#2415,.T.);
#1364=FACE_OUTER_BOUND('',#2416,.T.);
#1365=FACE_OUTER_BOUND('',#2417,.T.);
#1366=FACE_OUTER_BOUND('',#2418,.T.);
#1367=FACE_OUTER_BOUND('',#2419,.T.);
#1368=FACE_OUTER_BOUND('',#2420,.T.);
#1369=FACE_OUTER_BOUND('',#2421,.T.);
#1370=FACE_OUTER_BOUND('',#2422,.T.);
#1371=FACE_OUTER_BOUND('',#2423,.T.);
#1372=FACE_OUTER_BOUND('',#2424,.T.);
#1373=FACE_OUTER_BOUND('',#2425,.T.);
#1374=FACE_OUTER_BOUND('',#2426,.T.);
#1375=FACE_OUTER_BOUND('',#2427,.T.);
#1376=FACE_OUTER_BOUND('',#2428,.T.);
#1377=FACE_OUTER_BOUND('',#2429,.T.);
#1378=FACE_OUTER_BOUND('',#2430,.T.);
#1379=FACE_OUTER_BOUND('',#2431,.T.);
#1380=FACE_OUTER_BOUND('',#2432,.T.);
#1381=FACE_OUTER_BOUND('',#2433,.T.);
#1382=FACE_OUTER_BOUND('',#2434,.T.);
#1383=FACE_OUTER_BOUND('',#2437,.T.);
#1384=FACE_OUTER_BOUND('',#2438,.T.);
#1385=FACE_OUTER_BOUND('',#2439,.T.);
#1386=FACE_OUTER_BOUND('',#2440,.T.);
#1387=FACE_OUTER_BOUND('',#2441,.T.);
#1388=FACE_OUTER_BOUND('',#2442,.T.);
#1389=FACE_OUTER_BOUND('',#2443,.T.);
#1390=FACE_OUTER_BOUND('',#2446,.T.);
#1391=FACE_OUTER_BOUND('',#2447,.T.);
#1392=FACE_OUTER_BOUND('',#2448,.T.);
#1393=FACE_OUTER_BOUND('',#2449,.T.);
#1394=FACE_OUTER_BOUND('',#2450,.T.);
#1395=FACE_OUTER_BOUND('',#2451,.T.);
#1396=FACE_OUTER_BOUND('',#2452,.T.);
#1397=FACE_OUTER_BOUND('',#2453,.T.);
#1398=FACE_OUTER_BOUND('',#2456,.T.);
#1399=FACE_OUTER_BOUND('',#2457,.T.);
#1400=FACE_OUTER_BOUND('',#2458,.T.);
#1401=FACE_OUTER_BOUND('',#2459,.T.);
#1402=FACE_OUTER_BOUND('',#2460,.T.);
#1403=FACE_OUTER_BOUND('',#2461,.T.);
#1404=FACE_OUTER_BOUND('',#2462,.T.);
#1405=FACE_OUTER_BOUND('',#2463,.T.);
#1406=FACE_OUTER_BOUND('',#2464,.T.);
#1407=FACE_OUTER_BOUND('',#2467,.T.);
#1408=FACE_OUTER_BOUND('',#2468,.T.);
#1409=FACE_OUTER_BOUND('',#2469,.T.);
#1410=FACE_OUTER_BOUND('',#2470,.T.);
#1411=FACE_OUTER_BOUND('',#2471,.T.);
#1412=FACE_OUTER_BOUND('',#2472,.T.);
#1413=FACE_OUTER_BOUND('',#2473,.T.);
#1414=FACE_OUTER_BOUND('',#2474,.T.);
#1415=FACE_OUTER_BOUND('',#2475,.T.);
#1416=FACE_OUTER_BOUND('',#2476,.T.);
#1417=FACE_OUTER_BOUND('',#2477,.T.);
#1418=FACE_OUTER_BOUND('',#2478,.T.);
#1419=FACE_OUTER_BOUND('',#2479,.T.);
#1420=FACE_OUTER_BOUND('',#2480,.T.);
#1421=FACE_OUTER_BOUND('',#2481,.T.);
#1422=FACE_OUTER_BOUND('',#2482,.T.);
#1423=FACE_OUTER_BOUND('',#2483,.T.);
#1424=FACE_OUTER_BOUND('',#2484,.T.);
#1425=FACE_OUTER_BOUND('',#2485,.T.);
#1426=FACE_OUTER_BOUND('',#2486,.T.);
#1427=FACE_OUTER_BOUND('',#2487,.T.);
#1428=FACE_OUTER_BOUND('',#2488,.T.);
#1429=FACE_OUTER_BOUND('',#2489,.T.);
#1430=FACE_OUTER_BOUND('',#2490,.T.);
#1431=FACE_OUTER_BOUND('',#2491,.T.);
#1432=FACE_OUTER_BOUND('',#2492,.T.);
#1433=FACE_OUTER_BOUND('',#2493,.T.);
#1434=FACE_OUTER_BOUND('',#2494,.T.);
#1435=FACE_OUTER_BOUND('',#2495,.T.);
#1436=FACE_OUTER_BOUND('',#2496,.T.);
#1437=FACE_OUTER_BOUND('',#2497,.T.);
#1438=FACE_OUTER_BOUND('',#2498,.T.);
#1439=FACE_OUTER_BOUND('',#2499,.T.);
#1440=FACE_OUTER_BOUND('',#2500,.T.);
#1441=FACE_OUTER_BOUND('',#2501,.T.);
#1442=FACE_OUTER_BOUND('',#2502,.T.);
#1443=FACE_OUTER_BOUND('',#2503,.T.);
#1444=FACE_OUTER_BOUND('',#2504,.T.);
#1445=FACE_OUTER_BOUND('',#2505,.T.);
#1446=FACE_OUTER_BOUND('',#2506,.T.);
#1447=FACE_OUTER_BOUND('',#2507,.T.);
#1448=FACE_OUTER_BOUND('',#2508,.T.);
#1449=FACE_OUTER_BOUND('',#2509,.T.);
#1450=FACE_OUTER_BOUND('',#2510,.T.);
#1451=FACE_OUTER_BOUND('',#2511,.T.);
#1452=FACE_OUTER_BOUND('',#2512,.T.);
#1453=FACE_OUTER_BOUND('',#2513,.T.);
#1454=FACE_OUTER_BOUND('',#2514,.T.);
#1455=FACE_OUTER_BOUND('',#2515,.T.);
#1456=FACE_OUTER_BOUND('',#2516,.T.);
#1457=FACE_OUTER_BOUND('',#2517,.T.);
#1458=FACE_OUTER_BOUND('',#2518,.T.);
#2385=EDGE_LOOP('',(#13371,#13372,#13373,#13374,#13375,#13376,#13377,#13378,
#13379,#13380,#13381,#13382,#13383,#13384,#13385,#13386,#13387,#13388,#13389,
#13390,#13391,#13392,#13393,#13394,#13395,#13396,#13397,#13398,#13399,#13400,
#13401,#13402,#13403,#13404,#13405,#13406));
#2386=EDGE_LOOP('',(#13407,#13408,#13409,#13410));
#2387=EDGE_LOOP('',(#13411,#13412,#13413,#13414));
#2388=EDGE_LOOP('',(#13415,#13416,#13417,#13418));
#2389=EDGE_LOOP('',(#13419,#13420,#13421,#13422));
#2390=EDGE_LOOP('',(#13423,#13424,#13425,#13426));
#2391=EDGE_LOOP('',(#13427,#13428,#13429,#13430));
#2392=EDGE_LOOP('',(#13431,#13432,#13433,#13434));
#2393=EDGE_LOOP('',(#13435,#13436,#13437,#13438));
#2394=EDGE_LOOP('',(#13439,#13440,#13441,#13442));
#2395=EDGE_LOOP('',(#13443,#13444,#13445,#13446));
#2396=EDGE_LOOP('',(#13447,#13448,#13449,#13450));
#2397=EDGE_LOOP('',(#13451,#13452,#13453,#13454));
#2398=EDGE_LOOP('',(#13455,#13456,#13457,#13458));
#2399=EDGE_LOOP('',(#13459,#13460,#13461,#13462));
#2400=EDGE_LOOP('',(#13463,#13464,#13465,#13466));
#2401=EDGE_LOOP('',(#13467,#13468,#13469,#13470));
#2402=EDGE_LOOP('',(#13471,#13472,#13473,#13474));
#2403=EDGE_LOOP('',(#13475,#13476,#13477,#13478));
#2404=EDGE_LOOP('',(#13479,#13480,#13481,#13482));
#2405=EDGE_LOOP('',(#13483,#13484,#13485,#13486));
#2406=EDGE_LOOP('',(#13487,#13488,#13489,#13490));
#2407=EDGE_LOOP('',(#13491,#13492,#13493,#13494));
#2408=EDGE_LOOP('',(#13495,#13496,#13497,#13498));
#2409=EDGE_LOOP('',(#13499,#13500,#13501,#13502));
#2410=EDGE_LOOP('',(#13503,#13504,#13505,#13506));
#2411=EDGE_LOOP('',(#13507,#13508,#13509,#13510));
#2412=EDGE_LOOP('',(#13511,#13512,#13513,#13514));
#2413=EDGE_LOOP('',(#13515,#13516,#13517,#13518));
#2414=EDGE_LOOP('',(#13519,#13520,#13521,#13522));
#2415=EDGE_LOOP('',(#13523,#13524,#13525,#13526));
#2416=EDGE_LOOP('',(#13527,#13528,#13529,#13530));
#2417=EDGE_LOOP('',(#13531,#13532,#13533,#13534));
#2418=EDGE_LOOP('',(#13535,#13536,#13537,#13538));
#2419=EDGE_LOOP('',(#13539,#13540,#13541,#13542));
#2420=EDGE_LOOP('',(#13543,#13544,#13545,#13546));
#2421=EDGE_LOOP('',(#13547,#13548,#13549,#13550));
#2422=EDGE_LOOP('',(#13551,#13552,#13553,#13554,#13555,#13556,#13557,#13558,
#13559,#13560,#13561,#13562,#13563,#13564,#13565,#13566,#13567,#13568,#13569,
#13570,#13571,#13572,#13573,#13574,#13575,#13576,#13577,#13578,#13579,#13580,
#13581,#13582,#13583,#13584,#13585,#13586));
#2423=EDGE_LOOP('',(#13587,#13588,#13589,#13590));
#2424=EDGE_LOOP('',(#13591,#13592,#13593,#13594));
#2425=EDGE_LOOP('',(#13595,#13596,#13597,#13598));
#2426=EDGE_LOOP('',(#13599,#13600,#13601,#13602));
#2427=EDGE_LOOP('',(#13603,#13604,#13605,#13606));
#2428=EDGE_LOOP('',(#13607,#13608,#13609,#13610));
#2429=EDGE_LOOP('',(#13611,#13612,#13613,#13614));
#2430=EDGE_LOOP('',(#13615,#13616,#13617,#13618,#13619,#13620,#13621,#13622,
#13623,#13624,#13625,#13626,#13627,#13628,#13629,#13630,#13631,#13632,#13633,
#13634,#13635,#13636,#13637,#13638,#13639,#13640,#13641,#13642,#13643,#13644,
#13645,#13646,#13647,#13648,#13649,#13650,#13651,#13652,#13653,#13654,#13655,
#13656,#13657,#13658));
#2431=EDGE_LOOP('',(#13659,#13660,#13661,#13662));
#2432=EDGE_LOOP('',(#13663,#13664,#13665,#13666));
#2433=EDGE_LOOP('',(#13667,#13668,#13669,#13670));
#2434=EDGE_LOOP('',(#13671,#13672,#13673,#13674));
#2435=EDGE_LOOP('',(#13675));
#2436=EDGE_LOOP('',(#13676));
#2437=EDGE_LOOP('',(#13677,#13678,#13679,#13680));
#2438=EDGE_LOOP('',(#13681,#13682,#13683,#13684));
#2439=EDGE_LOOP('',(#13685,#13686,#13687,#13688,#13689,#13690,#13691,#13692,
#13693,#13694,#13695,#13696,#13697,#13698,#13699,#13700,#13701,#13702,#13703,
#13704,#13705,#13706,#13707,#13708,#13709,#13710,#13711,#13712,#13713,#13714,
#13715,#13716,#13717,#13718,#13719,#13720,#13721,#13722,#13723,#13724,#13725,
#13726,#13727,#13728));
#2440=EDGE_LOOP('',(#13729,#13730,#13731,#13732));
#2441=EDGE_LOOP('',(#13733,#13734,#13735,#13736));
#2442=EDGE_LOOP('',(#13737,#13738,#13739,#13740));
#2443=EDGE_LOOP('',(#13741,#13742,#13743,#13744));
#2444=EDGE_LOOP('',(#13745));
#2445=EDGE_LOOP('',(#13746));
#2446=EDGE_LOOP('',(#13747,#13748,#13749,#13750));
#2447=EDGE_LOOP('',(#13751,#13752,#13753,#13754));
#2448=EDGE_LOOP('',(#13755,#13756,#13757,#13758));
#2449=EDGE_LOOP('',(#13759,#13760,#13761,#13762));
#2450=EDGE_LOOP('',(#13763,#13764,#13765,#13766));
#2451=EDGE_LOOP('',(#13767,#13768,#13769,#13770));
#2452=EDGE_LOOP('',(#13771,#13772,#13773,#13774));
#2453=EDGE_LOOP('',(#13775,#13776,#13777,#13778));
#2454=EDGE_LOOP('',(#13779));
#2455=EDGE_LOOP('',(#13780));
#2456=EDGE_LOOP('',(#13781,#13782,#13783,#13784));
#2457=EDGE_LOOP('',(#13785,#13786,#13787,#13788));
#2458=EDGE_LOOP('',(#13789,#13790,#13791,#13792));
#2459=EDGE_LOOP('',(#13793,#13794,#13795,#13796));
#2460=EDGE_LOOP('',(#13797,#13798,#13799,#13800));
#2461=EDGE_LOOP('',(#13801,#13802,#13803,#13804));
#2462=EDGE_LOOP('',(#13805,#13806,#13807,#13808));
#2463=EDGE_LOOP('',(#13809,#13810,#13811,#13812));
#2464=EDGE_LOOP('',(#13813,#13814,#13815,#13816));
#2465=EDGE_LOOP('',(#13817));
#2466=EDGE_LOOP('',(#13818));
#2467=EDGE_LOOP('',(#13819,#13820,#13821,#13822));
#2468=EDGE_LOOP('',(#13823,#13824,#13825,#13826));
#2469=EDGE_LOOP('',(#13827,#13828,#13829,#13830));
#2470=EDGE_LOOP('',(#13831,#13832,#13833,#13834));
#2471=EDGE_LOOP('',(#13835,#13836,#13837,#13838));
#2472=EDGE_LOOP('',(#13839,#13840,#13841,#13842));
#2473=EDGE_LOOP('',(#13843,#13844,#13845,#13846));
#2474=EDGE_LOOP('',(#13847,#13848,#13849,#13850));
#2475=EDGE_LOOP('',(#13851,#13852,#13853,#13854));
#2476=EDGE_LOOP('',(#13855,#13856,#13857,#13858));
#2477=EDGE_LOOP('',(#13859,#13860,#13861,#13862));
#2478=EDGE_LOOP('',(#13863,#13864,#13865,#13866));
#2479=EDGE_LOOP('',(#13867,#13868,#13869,#13870));
#2480=EDGE_LOOP('',(#13871,#13872,#13873,#13874));
#2481=EDGE_LOOP('',(#13875,#13876,#13877,#13878));
#2482=EDGE_LOOP('',(#13879,#13880,#13881,#13882));
#2483=EDGE_LOOP('',(#13883,#13884,#13885,#13886));
#2484=EDGE_LOOP('',(#13887,#13888,#13889,#13890));
#2485=EDGE_LOOP('',(#13891,#13892,#13893,#13894));
#2486=EDGE_LOOP('',(#13895,#13896,#13897,#13898));
#2487=EDGE_LOOP('',(#13899,#13900,#13901,#13902));
#2488=EDGE_LOOP('',(#13903,#13904,#13905,#13906));
#2489=EDGE_LOOP('',(#13907,#13908,#13909,#13910));
#2490=EDGE_LOOP('',(#13911,#13912,#13913,#13914));
#2491=EDGE_LOOP('',(#13915,#13916,#13917,#13918));
#2492=EDGE_LOOP('',(#13919,#13920,#13921,#13922));
#2493=EDGE_LOOP('',(#13923,#13924,#13925,#13926));
#2494=EDGE_LOOP('',(#13927,#13928,#13929,#13930));
#2495=EDGE_LOOP('',(#13931,#13932,#13933,#13934));
#2496=EDGE_LOOP('',(#13935,#13936,#13937,#13938));
#2497=EDGE_LOOP('',(#13939,#13940,#13941,#13942,#13943,#13944,#13945,#13946,
#13947,#13948,#13949,#13950,#13951,#13952,#13953,#13954,#13955,#13956,#13957,
#13958,#13959,#13960,#13961,#13962,#13963,#13964,#13965,#13966,#13967,#13968,
#13969,#13970,#13971,#13972,#13973,#13974));
#2498=EDGE_LOOP('',(#13975,#13976,#13977,#13978));
#2499=EDGE_LOOP('',(#13979,#13980,#13981,#13982));
#2500=EDGE_LOOP('',(#13983,#13984,#13985,#13986));
#2501=EDGE_LOOP('',(#13987,#13988,#13989,#13990));
#2502=EDGE_LOOP('',(#13991,#13992,#13993,#13994));
#2503=EDGE_LOOP('',(#13995,#13996,#13997,#13998));
#2504=EDGE_LOOP('',(#13999,#14000,#14001,#14002));
#2505=EDGE_LOOP('',(#14003,#14004,#14005,#14006));
#2506=EDGE_LOOP('',(#14007,#14008,#14009,#14010));
#2507=EDGE_LOOP('',(#14011,#14012,#14013,#14014));
#2508=EDGE_LOOP('',(#14015,#14016,#14017,#14018));
#2509=EDGE_LOOP('',(#14019,#14020,#14021,#14022));
#2510=EDGE_LOOP('',(#14023,#14024,#14025,#14026));
#2511=EDGE_LOOP('',(#14027,#14028,#14029,#14030));
#2512=EDGE_LOOP('',(#14031,#14032,#14033,#14034));
#2513=EDGE_LOOP('',(#14035,#14036,#14037,#14038));
#2514=EDGE_LOOP('',(#14039,#14040,#14041,#14042));
#2515=EDGE_LOOP('',(#14043,#14044,#14045,#14046));
#2516=EDGE_LOOP('',(#14047,#14048,#14049,#14050));
#2517=EDGE_LOOP('',(#14051,#14052,#14053,#14054));
#2518=EDGE_LOOP('',(#14055,#14056,#14057,#14058,#14059,#14060,#14061,#14062,
#14063,#14064,#14065,#14066,#14067,#14068,#14069,#14070,#14071,#14072,#14073,
#14074,#14075,#14076,#14077,#14078,#14079,#14080,#14081,#14082,#14083,#14084,
#14085,#14086,#14087,#14088,#14089,#14090));
#3497=CIRCLE('',#20494,1.04999999999981);
#3498=CIRCLE('',#20495,1.04999999999995);
#3499=CIRCLE('',#20496,1.39999999999995);
#3500=CIRCLE('',#20497,2.36402292474775);
#3501=CIRCLE('',#20498,0.59999999999997);
#3502=CIRCLE('',#20499,0.724999999999998);
#3503=CIRCLE('',#20500,2.46743797397104);
#3504=CIRCLE('',#20501,0.45000000000016);
#3505=CIRCLE('',#20502,0.450000000000123);
#3506=CIRCLE('',#20503,2.46743797397101);
#3507=CIRCLE('',#20504,0.72500000000001);
#3508=CIRCLE('',#20505,0.599999999999987);
#3509=CIRCLE('',#20506,2.3640229247478);
#3510=CIRCLE('',#20507,1.39999999999978);
#3511=CIRCLE('',#20508,1.05);
#3512=CIRCLE('',#20509,1.04999999999996);
#3513=CIRCLE('',#20512,0.45000000000016);
#3514=CIRCLE('',#20514,2.46743797397104);
#3515=CIRCLE('',#20516,0.724999999999998);
#3516=CIRCLE('',#20519,0.59999999999997);
#3517=CIRCLE('',#20521,2.36402292474775);
#3518=CIRCLE('',#20523,1.39999999999995);
#3519=CIRCLE('',#20526,1.04999999999995);
#3520=CIRCLE('',#20529,1.04999999999981);
#3521=CIRCLE('',#20539,1.04999999999996);
#3522=CIRCLE('',#20547,0.450000000000123);
#3523=CIRCLE('',#20549,2.46743797397101);
#3524=CIRCLE('',#20551,0.72500000000001);
#3525=CIRCLE('',#20554,0.599999999999987);
#3526=CIRCLE('',#20556,2.3640229247478);
#3527=CIRCLE('',#20558,1.39999999999978);
#3528=CIRCLE('',#20561,1.05);
#3529=CIRCLE('',#20565,0.45000000000016);
#3530=CIRCLE('',#20566,0.45000000000016);
#3531=CIRCLE('',#20568,2.46743797397104);
#3532=CIRCLE('',#20569,2.46743797397104);
#3533=CIRCLE('',#20571,0.724999999999998);
#3534=CIRCLE('',#20572,0.724999999999998);
#3535=CIRCLE('',#20575,0.59999999999997);
#3536=CIRCLE('',#20576,0.59999999999997);
#3537=CIRCLE('',#20578,2.36402292474775);
#3538=CIRCLE('',#20579,2.36402292474775);
#3539=CIRCLE('',#20581,2.16656587073651);
#3540=CIRCLE('',#20582,2.16656587073651);
#3541=CIRCLE('',#20583,1.04999999999996);
#3542=CIRCLE('',#20584,1.05);
#3543=CIRCLE('',#20585,1.39999999999978);
#3544=CIRCLE('',#20586,2.3640229247478);
#3545=CIRCLE('',#20587,0.599999999999987);
#3546=CIRCLE('',#20588,0.72500000000001);
#3547=CIRCLE('',#20589,2.46743797397101);
#3548=CIRCLE('',#20590,0.450000000000123);
#3549=CIRCLE('',#20591,1.39999999999995);
#3550=CIRCLE('',#20592,1.04999999999995);
#3551=CIRCLE('',#20593,1.04999999999981);
#3552=CIRCLE('',#20598,3.00000000000001);
#3553=CIRCLE('',#20599,3.00000000000001);
#3554=CIRCLE('',#20601,2.16656587073651);
#3555=CIRCLE('',#20604,1.04999999999981);
#3556=CIRCLE('',#20605,1.04999999999995);
#3557=CIRCLE('',#20606,1.39999999999995);
#3558=CIRCLE('',#20607,0.450000000000123);
#3559=CIRCLE('',#20608,2.46743797397101);
#3560=CIRCLE('',#20609,0.72500000000001);
#3561=CIRCLE('',#20610,0.599999999999987);
#3562=CIRCLE('',#20611,2.3640229247478);
#3563=CIRCLE('',#20612,1.39999999999978);
#3564=CIRCLE('',#20613,1.05);
#3565=CIRCLE('',#20614,1.04999999999996);
#3566=CIRCLE('',#20615,2.16656587073651);
#3567=CIRCLE('',#20620,3.00000000000001);
#3568=CIRCLE('',#20621,3.00000000000001);
#3569=CIRCLE('',#20624,3.00000000000001);
#3570=CIRCLE('',#20626,3.00000000000001);
#3571=CIRCLE('',#20628,3.00000000000001);
#3572=CIRCLE('',#20630,3.00000000000001);
#3573=CIRCLE('',#20658,1.39999999999995);
#3574=CIRCLE('',#20659,1.39999999999995);
#3575=CIRCLE('',#20662,1.04999999999995);
#3576=CIRCLE('',#20663,1.04999999999995);
#3577=CIRCLE('',#20666,1.04999999999981);
#3578=CIRCLE('',#20667,1.04999999999981);
#3579=CIRCLE('',#20679,1.04999999999996);
#3580=CIRCLE('',#20680,1.04999999999996);
#3581=CIRCLE('',#20682,1.05);
#3582=CIRCLE('',#20683,2.36402292474775);
#3583=CIRCLE('',#20684,0.59999999999997);
#3584=CIRCLE('',#20685,0.724999999999998);
#3585=CIRCLE('',#20686,2.46743797397104);
#3586=CIRCLE('',#20687,0.45000000000016);
#3587=CIRCLE('',#20688,0.450000000000123);
#3588=CIRCLE('',#20689,2.46743797397101);
#3589=CIRCLE('',#20690,0.72500000000001);
#3590=CIRCLE('',#20691,0.599999999999987);
#3591=CIRCLE('',#20692,2.3640229247478);
#3592=CIRCLE('',#20693,1.39999999999978);
#3593=CIRCLE('',#20697,1.05);
#3594=CIRCLE('',#20700,1.39999999999978);
#3595=CIRCLE('',#20702,2.3640229247478);
#3596=CIRCLE('',#20704,0.599999999999987);
#3597=CIRCLE('',#20707,0.72500000000001);
#3598=CIRCLE('',#20709,2.46743797397101);
#3599=CIRCLE('',#20711,0.450000000000123);
#3600=CIRCLE('',#20716,0.45000000000016);
#3601=CIRCLE('',#20718,2.46743797397104);
#3602=CIRCLE('',#20720,0.724999999999998);
#3603=CIRCLE('',#20723,0.59999999999997);
#3604=CIRCLE('',#20725,2.36402292474775);
#4245=LINE('',#27879,#6126);
#4246=LINE('',#27881,#6127);
#4247=LINE('',#27883,#6128);
#4248=LINE('',#27885,#6129);
#4249=LINE('',#27887,#6130);
#4250=LINE('',#27889,#6131);
#4251=LINE('',#27891,#6132);
#4252=LINE('',#27893,#6133);
#4253=LINE('',#27897,#6134);
#4254=LINE('',#27901,#6135);
#4255=LINE('',#27909,#6136);
#4256=LINE('',#27917,#6137);
#4257=LINE('',#27919,#6138);
#4258=LINE('',#27921,#6139);
#4259=LINE('',#27929,#6140);
#4260=LINE('',#27937,#6141);
#4261=LINE('',#27941,#6142);
#4262=LINE('',#27945,#6143);
#4263=LINE('',#27947,#6144);
#4264=LINE('',#27948,#6145);
#4265=LINE('',#27951,#6146);
#4266=LINE('',#27953,#6147);
#4267=LINE('',#27954,#6148);
#4268=LINE('',#27957,#6149);
#4269=LINE('',#27961,#6150);
#4270=LINE('',#27965,#6151);
#4271=LINE('',#27969,#6152);
#4272=LINE('',#27970,#6153);
#4273=LINE('',#27973,#6154);
#4274=LINE('',#27977,#6155);
#4275=LINE('',#27981,#6156);
#4276=LINE('',#27985,#6157);
#4277=LINE('',#27986,#6158);
#4278=LINE('',#27989,#6159);
#4279=LINE('',#27993,#6160);
#4280=LINE('',#27994,#6161);
#4281=LINE('',#27997,#6162);
#4282=LINE('',#28001,#6163);
#4283=LINE('',#28002,#6164);
#4284=LINE('',#28005,#6165);
#4285=LINE('',#28006,#6166);
#4286=LINE('',#28009,#6167);
#4287=LINE('',#28010,#6168);
#4288=LINE('',#28013,#6169);
#4289=LINE('',#28014,#6170);
#4290=LINE('',#28017,#6171);
#4291=LINE('',#28019,#6172);
#4292=LINE('',#28020,#6173);
#4293=LINE('',#28023,#6174);
#4294=LINE('',#28024,#6175);
#4295=LINE('',#28027,#6176);
#4296=LINE('',#28028,#6177);
#4297=LINE('',#28031,#6178);
#4298=LINE('',#28032,#6179);
#4299=LINE('',#28035,#6180);
#4300=LINE('',#28039,#6181);
#4301=LINE('',#28040,#6182);
#4302=LINE('',#28043,#6183);
#4303=LINE('',#28044,#6184);
#4304=LINE('',#28046,#6185);
#4305=LINE('',#28049,#6186);
#4306=LINE('',#28050,#6187);
#4307=LINE('',#28053,#6188);
#4308=LINE('',#28054,#6189);
#4309=LINE('',#28057,#6190);
#4310=LINE('',#28058,#6191);
#4311=LINE('',#28062,#6192);
#4312=LINE('',#28066,#6193);
#4313=LINE('',#28070,#6194);
#4314=LINE('',#28073,#6195);
#4315=LINE('',#28074,#6196);
#4316=LINE('',#28078,#6197);
#4317=LINE('',#28082,#6198);
#4318=LINE('',#28086,#6199);
#4319=LINE('',#28089,#6200);
#4320=LINE('',#28090,#6201);
#4321=LINE('',#28097,#6202);
#4322=LINE('',#28099,#6203);
#4323=LINE('',#28101,#6204);
#4324=LINE('',#28102,#6205);
#4325=LINE('',#28108,#6206);
#4326=LINE('',#28114,#6207);
#4327=LINE('',#28120,#6208);
#4328=LINE('',#28123,#6209);
#4329=LINE('',#28125,#6210);
#4330=LINE('',#28126,#6211);
#4331=LINE('',#28132,#6212);
#4332=LINE('',#28138,#6213);
#4333=LINE('',#28142,#6214);
#4334=LINE('',#28144,#6215);
#4335=LINE('',#28146,#6216);
#4336=LINE('',#28148,#6217);
#4337=LINE('',#28152,#6218);
#4338=LINE('',#28156,#6219);
#4339=LINE('',#28158,#6220);
#4340=LINE('',#28160,#6221);
#4341=LINE('',#28162,#6222);
#4342=LINE('',#28164,#6223);
#4343=LINE('',#28166,#6224);
#4344=LINE('',#28168,#6225);
#4345=LINE('',#28170,#6226);
#4346=LINE('',#28174,#6227);
#4347=LINE('',#28178,#6228);
#4348=LINE('',#28186,#6229);
#4349=LINE('',#28194,#6230);
#4350=LINE('',#28195,#6231);
#4351=LINE('',#28199,#6232);
#4352=LINE('',#28203,#6233);
#4353=LINE('',#28207,#6234);
#4354=LINE('',#28209,#6235);
#4355=LINE('',#28211,#6236);
#4356=LINE('',#28212,#6237);
#4357=LINE('',#28215,#6238);
#4358=LINE('',#28217,#6239);
#4359=LINE('',#28218,#6240);
#4360=LINE('',#28221,#6241);
#4361=LINE('',#28222,#6242);
#4362=LINE('',#28225,#6243);
#4363=LINE('',#28226,#6244);
#4364=LINE('',#28229,#6245);
#4365=LINE('',#28230,#6246);
#4366=LINE('',#28237,#6247);
#4367=LINE('',#28241,#6248);
#4368=LINE('',#28242,#6249);
#4369=LINE('',#28245,#6250);
#4370=LINE('',#28247,#6251);
#4371=LINE('',#28249,#6252);
#4372=LINE('',#28251,#6253);
#4373=LINE('',#28255,#6254);
#4374=LINE('',#28259,#6255);
#4375=LINE('',#28262,#6256);
#4376=LINE('',#28264,#6257);
#4377=LINE('',#28272,#6258);
#4378=LINE('',#28280,#6259);
#4379=LINE('',#28284,#6260);
#4380=LINE('',#28288,#6261);
#4381=LINE('',#28290,#6262);
#4382=LINE('',#28292,#6263);
#4383=LINE('',#28294,#6264);
#4384=LINE('',#28296,#6265);
#4385=LINE('',#28298,#6266);
#4386=LINE('',#28300,#6267);
#4387=LINE('',#28302,#6268);
#4388=LINE('',#28305,#6269);
#4389=LINE('',#28306,#6270);
#4390=LINE('',#28308,#6271);
#4391=LINE('',#28310,#6272);
#4392=LINE('',#28312,#6273);
#4393=LINE('',#28320,#6274);
#4394=LINE('',#28324,#6275);
#4395=LINE('',#28328,#6276);
#4396=LINE('',#28332,#6277);
#4397=LINE('',#28335,#6278);
#4398=LINE('',#28337,#6279);
#4399=LINE('',#28339,#6280);
#4400=LINE('',#28341,#6281);
#4401=LINE('',#28343,#6282);
#4402=LINE('',#28345,#6283);
#4403=LINE('',#28347,#6284);
#4404=LINE('',#28349,#6285);
#4405=LINE('',#28352,#6286);
#4406=LINE('',#28354,#6287);
#4407=LINE('',#28356,#6288);
#4408=LINE('',#28358,#6289);
#4409=LINE('',#28360,#6290);
#4410=LINE('',#28362,#6291);
#4411=LINE('',#28364,#6292);
#4412=LINE('',#28366,#6293);
#4413=LINE('',#28368,#6294);
#4414=LINE('',#28370,#6295);
#4415=LINE('',#28372,#6296);
#4416=LINE('',#28374,#6297);
#4417=LINE('',#28376,#6298);
#4418=LINE('',#28378,#6299);
#4419=LINE('',#28380,#6300);
#4420=LINE('',#28382,#6301);
#4421=LINE('',#28389,#6302);
#4422=LINE('',#28392,#6303);
#4423=LINE('',#28395,#6304);
#4424=LINE('',#28397,#6305);
#4425=LINE('',#28398,#6306);
#4426=LINE('',#28404,#6307);
#4427=LINE('',#28407,#6308);
#4428=LINE('',#28409,#6309);
#4429=LINE('',#28410,#6310);
#4430=LINE('',#28416,#6311);
#4431=LINE('',#28419,#6312);
#4432=LINE('',#28421,#6313);
#4433=LINE('',#28422,#6314);
#4434=LINE('',#28425,#6315);
#4435=LINE('',#28427,#6316);
#4436=LINE('',#28428,#6317);
#4437=LINE('',#28431,#6318);
#4438=LINE('',#28433,#6319);
#4439=LINE('',#28434,#6320);
#4440=LINE('',#28438,#6321);
#4441=LINE('',#28440,#6322);
#4442=LINE('',#28442,#6323);
#4443=LINE('',#28443,#6324);
#4444=LINE('',#28446,#6325);
#4445=LINE('',#28448,#6326);
#4446=LINE('',#28449,#6327);
#4447=LINE('',#28452,#6328);
#4448=LINE('',#28454,#6329);
#4449=LINE('',#28455,#6330);
#4450=LINE('',#28458,#6331);
#4451=LINE('',#28460,#6332);
#4452=LINE('',#28461,#6333);
#4453=LINE('',#28464,#6334);
#4454=LINE('',#28466,#6335);
#4455=LINE('',#28467,#6336);
#4456=LINE('',#28470,#6337);
#4457=LINE('',#28472,#6338);
#4458=LINE('',#28473,#6339);
#4459=LINE('',#28476,#6340);
#4460=LINE('',#28478,#6341);
#4461=LINE('',#28479,#6342);
#4462=LINE('',#28485,#6343);
#4463=LINE('',#28490,#6344);
#4464=LINE('',#28491,#6345);
#4465=LINE('',#28497,#6346);
#4466=LINE('',#28505,#6347);
#4467=LINE('',#28507,#6348);
#4468=LINE('',#28509,#6349);
#4469=LINE('',#28517,#6350);
#4470=LINE('',#28524,#6351);
#4471=LINE('',#28526,#6352);
#4472=LINE('',#28529,#6353);
#4473=LINE('',#28530,#6354);
#4474=LINE('',#28534,#6355);
#4475=LINE('',#28537,#6356);
#4476=LINE('',#28538,#6357);
#4477=LINE('',#28542,#6358);
#4478=LINE('',#28546,#6359);
#4479=LINE('',#28550,#6360);
#4480=LINE('',#28553,#6361);
#4481=LINE('',#28554,#6362);
#4482=LINE('',#28558,#6363);
#4483=LINE('',#28562,#6364);
#4484=LINE('',#28566,#6365);
#4485=LINE('',#28569,#6366);
#4486=LINE('',#28570,#6367);
#4487=LINE('',#28573,#6368);
#4488=LINE('',#28574,#6369);
#4489=LINE('',#28577,#6370);
#4490=LINE('',#28578,#6371);
#4491=LINE('',#28582,#6372);
#4492=LINE('',#28586,#6373);
#4493=LINE('',#28590,#6374);
#4494=LINE('',#28593,#6375);
#4495=LINE('',#28594,#6376);
#4496=LINE('',#28598,#6377);
#6126=VECTOR('',#22654,10.);
#6127=VECTOR('',#22655,10.);
#6128=VECTOR('',#22656,10.);
#6129=VECTOR('',#22657,10.);
#6130=VECTOR('',#22658,10.);
#6131=VECTOR('',#22659,10.);
#6132=VECTOR('',#22660,10.);
#6133=VECTOR('',#22661,10.);
#6134=VECTOR('',#22664,10.);
#6135=VECTOR('',#22667,10.);
#6136=VECTOR('',#22674,10.);
#6137=VECTOR('',#22681,10.);
#6138=VECTOR('',#22682,10.);
#6139=VECTOR('',#22683,10.);
#6140=VECTOR('',#22690,10.);
#6141=VECTOR('',#22697,10.);
#6142=VECTOR('',#22700,10.);
#6143=VECTOR('',#22703,10.);
#6144=VECTOR('',#22704,10.);
#6145=VECTOR('',#22705,10.);
#6146=VECTOR('',#22708,10.);
#6147=VECTOR('',#22709,10.);
#6148=VECTOR('',#22710,10.);
#6149=VECTOR('',#22713,10.);
#6150=VECTOR('',#22718,10.);
#6151=VECTOR('',#22723,10.);
#6152=VECTOR('',#22728,10.);
#6153=VECTOR('',#22729,10.);
#6154=VECTOR('',#22732,10.);
#6155=VECTOR('',#22737,10.);
#6156=VECTOR('',#22742,10.);
#6157=VECTOR('',#22747,10.);
#6158=VECTOR('',#22748,10.);
#6159=VECTOR('',#22751,10.);
#6160=VECTOR('',#22756,10.);
#6161=VECTOR('',#22757,10.);
#6162=VECTOR('',#22760,10.);
#6163=VECTOR('',#22765,10.);
#6164=VECTOR('',#22766,10.);
#6165=VECTOR('',#22769,10.);
#6166=VECTOR('',#22770,10.);
#6167=VECTOR('',#22773,10.);
#6168=VECTOR('',#22774,10.);
#6169=VECTOR('',#22777,10.);
#6170=VECTOR('',#22778,10.);
#6171=VECTOR('',#22781,10.);
#6172=VECTOR('',#22782,10.);
#6173=VECTOR('',#22783,10.);
#6174=VECTOR('',#22786,10.);
#6175=VECTOR('',#22787,10.);
#6176=VECTOR('',#22790,10.);
#6177=VECTOR('',#22791,10.);
#6178=VECTOR('',#22794,10.);
#6179=VECTOR('',#22795,10.);
#6180=VECTOR('',#22798,10.);
#6181=VECTOR('',#22803,10.);
#6182=VECTOR('',#22804,10.);
#6183=VECTOR('',#22807,10.);
#6184=VECTOR('',#22808,10.);
#6185=VECTOR('',#22811,10.);
#6186=VECTOR('',#22814,10.);
#6187=VECTOR('',#22815,10.);
#6188=VECTOR('',#22818,10.);
#6189=VECTOR('',#22819,10.);
#6190=VECTOR('',#22822,10.);
#6191=VECTOR('',#22823,10.);
#6192=VECTOR('',#22828,10.);
#6193=VECTOR('',#22833,10.);
#6194=VECTOR('',#22838,10.);
#6195=VECTOR('',#22841,10.);
#6196=VECTOR('',#22842,10.);
#6197=VECTOR('',#22847,10.);
#6198=VECTOR('',#22852,10.);
#6199=VECTOR('',#22857,10.);
#6200=VECTOR('',#22860,10.);
#6201=VECTOR('',#22861,10.);
#6202=VECTOR('',#22870,10.);
#6203=VECTOR('',#22871,10.);
#6204=VECTOR('',#22872,10.);
#6205=VECTOR('',#22873,10.);
#6206=VECTOR('',#22880,10.);
#6207=VECTOR('',#22887,10.);
#6208=VECTOR('',#22894,10.);
#6209=VECTOR('',#22897,10.);
#6210=VECTOR('',#22898,10.);
#6211=VECTOR('',#22899,10.);
#6212=VECTOR('',#22906,10.);
#6213=VECTOR('',#22913,10.);
#6214=VECTOR('',#22916,10.);
#6215=VECTOR('',#22917,10.);
#6216=VECTOR('',#22918,10.);
#6217=VECTOR('',#22919,10.);
#6218=VECTOR('',#22922,10.);
#6219=VECTOR('',#22925,10.);
#6220=VECTOR('',#22926,10.);
#6221=VECTOR('',#22927,10.);
#6222=VECTOR('',#22928,10.);
#6223=VECTOR('',#22929,10.);
#6224=VECTOR('',#22930,10.);
#6225=VECTOR('',#22931,10.);
#6226=VECTOR('',#22932,10.);
#6227=VECTOR('',#22935,10.);
#6228=VECTOR('',#22938,10.);
#6229=VECTOR('',#22945,10.);
#6230=VECTOR('',#22952,10.);
#6231=VECTOR('',#22953,10.);
#6232=VECTOR('',#22956,10.);
#6233=VECTOR('',#22959,10.);
#6234=VECTOR('',#22962,10.);
#6235=VECTOR('',#22963,10.);
#6236=VECTOR('',#22964,10.);
#6237=VECTOR('',#22965,10.);
#6238=VECTOR('',#22968,10.);
#6239=VECTOR('',#22969,10.);
#6240=VECTOR('',#22970,10.);
#6241=VECTOR('',#22973,10.);
#6242=VECTOR('',#22974,10.);
#6243=VECTOR('',#22977,10.);
#6244=VECTOR('',#22978,10.);
#6245=VECTOR('',#22981,10.);
#6246=VECTOR('',#22982,10.);
#6247=VECTOR('',#22989,10.);
#6248=VECTOR('',#22994,10.);
#6249=VECTOR('',#22995,10.);
#6250=VECTOR('',#22998,10.);
#6251=VECTOR('',#22999,10.);
#6252=VECTOR('',#23000,10.);
#6253=VECTOR('',#23001,10.);
#6254=VECTOR('',#23004,10.);
#6255=VECTOR('',#23007,10.);
#6256=VECTOR('',#23010,10.);
#6257=VECTOR('',#23011,10.);
#6258=VECTOR('',#23018,10.);
#6259=VECTOR('',#23025,10.);
#6260=VECTOR('',#23028,10.);
#6261=VECTOR('',#23031,10.);
#6262=VECTOR('',#23032,10.);
#6263=VECTOR('',#23033,10.);
#6264=VECTOR('',#23034,10.);
#6265=VECTOR('',#23035,10.);
#6266=VECTOR('',#23036,10.);
#6267=VECTOR('',#23037,10.);
#6268=VECTOR('',#23038,10.);
#6269=VECTOR('',#23043,10.);
#6270=VECTOR('',#23044,10.);
#6271=VECTOR('',#23047,10.);
#6272=VECTOR('',#23050,10.);
#6273=VECTOR('',#23053,10.);
#6274=VECTOR('',#23062,3.00000000000001);
#6275=VECTOR('',#23067,3.00000000000001);
#6276=VECTOR('',#23072,3.00000000000001);
#6277=VECTOR('',#23077,3.00000000000001);
#6278=VECTOR('',#23082,10.);
#6279=VECTOR('',#23085,10.);
#6280=VECTOR('',#23088,10.);
#6281=VECTOR('',#23091,10.);
#6282=VECTOR('',#23094,10.);
#6283=VECTOR('',#23097,10.);
#6284=VECTOR('',#23100,10.);
#6285=VECTOR('',#23103,10.);
#6286=VECTOR('',#23108,10.);
#6287=VECTOR('',#23111,10.);
#6288=VECTOR('',#23114,10.);
#6289=VECTOR('',#23117,10.);
#6290=VECTOR('',#23120,10.);
#6291=VECTOR('',#23123,10.);
#6292=VECTOR('',#23126,10.);
#6293=VECTOR('',#23129,10.);
#6294=VECTOR('',#23132,10.);
#6295=VECTOR('',#23135,10.);
#6296=VECTOR('',#23138,10.);
#6297=VECTOR('',#23141,10.);
#6298=VECTOR('',#23144,10.);
#6299=VECTOR('',#23147,10.);
#6300=VECTOR('',#23150,10.);
#6301=VECTOR('',#23153,10.);
#6302=VECTOR('',#23160,10.);
#6303=VECTOR('',#23163,10.);
#6304=VECTOR('',#23166,10.);
#6305=VECTOR('',#23167,10.);
#6306=VECTOR('',#23168,10.);
#6307=VECTOR('',#23175,10.);
#6308=VECTOR('',#23178,10.);
#6309=VECTOR('',#23179,10.);
#6310=VECTOR('',#23180,10.);
#6311=VECTOR('',#23187,10.);
#6312=VECTOR('',#23190,10.);
#6313=VECTOR('',#23191,10.);
#6314=VECTOR('',#23192,10.);
#6315=VECTOR('',#23195,10.);
#6316=VECTOR('',#23196,10.);
#6317=VECTOR('',#23197,10.);
#6318=VECTOR('',#23200,10.);
#6319=VECTOR('',#23201,10.);
#6320=VECTOR('',#23202,10.);
#6321=VECTOR('',#23205,10.);
#6322=VECTOR('',#23206,10.);
#6323=VECTOR('',#23207,10.);
#6324=VECTOR('',#23208,10.);
#6325=VECTOR('',#23211,10.);
#6326=VECTOR('',#23212,10.);
#6327=VECTOR('',#23213,10.);
#6328=VECTOR('',#23216,10.);
#6329=VECTOR('',#23217,10.);
#6330=VECTOR('',#23218,10.);
#6331=VECTOR('',#23221,10.);
#6332=VECTOR('',#23222,10.);
#6333=VECTOR('',#23223,10.);
#6334=VECTOR('',#23226,10.);
#6335=VECTOR('',#23227,10.);
#6336=VECTOR('',#23228,10.);
#6337=VECTOR('',#23231,10.);
#6338=VECTOR('',#23232,10.);
#6339=VECTOR('',#23233,10.);
#6340=VECTOR('',#23236,10.);
#6341=VECTOR('',#23237,10.);
#6342=VECTOR('',#23238,10.);
#6343=VECTOR('',#23245,10.);
#6344=VECTOR('',#23250,10.);
#6345=VECTOR('',#23251,10.);
#6346=VECTOR('',#23256,10.);
#6347=VECTOR('',#23263,10.);
#6348=VECTOR('',#23264,10.);
#6349=VECTOR('',#23265,10.);
#6350=VECTOR('',#23272,10.);
#6351=VECTOR('',#23279,10.);
#6352=VECTOR('',#23282,10.);
#6353=VECTOR('',#23285,10.);
#6354=VECTOR('',#23286,10.);
#6355=VECTOR('',#23291,10.);
#6356=VECTOR('',#23294,10.);
#6357=VECTOR('',#23295,10.);
#6358=VECTOR('',#23300,10.);
#6359=VECTOR('',#23305,10.);
#6360=VECTOR('',#23310,10.);
#6361=VECTOR('',#23313,10.);
#6362=VECTOR('',#23314,10.);
#6363=VECTOR('',#23319,10.);
#6364=VECTOR('',#23324,10.);
#6365=VECTOR('',#23329,10.);
#6366=VECTOR('',#23332,10.);
#6367=VECTOR('',#23333,10.);
#6368=VECTOR('',#23336,10.);
#6369=VECTOR('',#23337,10.);
#6370=VECTOR('',#23340,10.);
#6371=VECTOR('',#23341,10.);
#6372=VECTOR('',#23346,10.);
#6373=VECTOR('',#23351,10.);
#6374=VECTOR('',#23356,10.);
#6375=VECTOR('',#23359,10.);
#6376=VECTOR('',#23360,10.);
#6377=VECTOR('',#23365,10.);
#7995=VERTEX_POINT('',#27877);
#7996=VERTEX_POINT('',#27878);
#7997=VERTEX_POINT('',#27880);
#7998=VERTEX_POINT('',#27882);
#7999=VERTEX_POINT('',#27884);
#8000=VERTEX_POINT('',#27886);
#8001=VERTEX_POINT('',#27888);
#8002=VERTEX_POINT('',#27890);
#8003=VERTEX_POINT('',#27892);
#8004=VERTEX_POINT('',#27894);
#8005=VERTEX_POINT('',#27896);
#8006=VERTEX_POINT('',#27898);
#8007=VERTEX_POINT('',#27900);
#8008=VERTEX_POINT('',#27902);
#8009=VERTEX_POINT('',#27904);
#8010=VERTEX_POINT('',#27906);
#8011=VERTEX_POINT('',#27908);
#8012=VERTEX_POINT('',#27910);
#8013=VERTEX_POINT('',#27912);
#8014=VERTEX_POINT('',#27914);
#8015=VERTEX_POINT('',#27916);
#8016=VERTEX_POINT('',#27918);
#8017=VERTEX_POINT('',#27920);
#8018=VERTEX_POINT('',#27922);
#8019=VERTEX_POINT('',#27924);
#8020=VERTEX_POINT('',#27926);
#8021=VERTEX_POINT('',#27928);
#8022=VERTEX_POINT('',#27930);
#8023=VERTEX_POINT('',#27932);
#8024=VERTEX_POINT('',#27934);
#8025=VERTEX_POINT('',#27936);
#8026=VERTEX_POINT('',#27938);
#8027=VERTEX_POINT('',#27940);
#8028=VERTEX_POINT('',#27942);
#8029=VERTEX_POINT('',#27944);
#8030=VERTEX_POINT('',#27946);
#8031=VERTEX_POINT('',#27950);
#8032=VERTEX_POINT('',#27952);
#8033=VERTEX_POINT('',#27956);
#8034=VERTEX_POINT('',#27960);
#8035=VERTEX_POINT('',#27964);
#8036=VERTEX_POINT('',#27968);
#8037=VERTEX_POINT('',#27972);
#8038=VERTEX_POINT('',#27976);
#8039=VERTEX_POINT('',#27980);
#8040=VERTEX_POINT('',#27984);
#8041=VERTEX_POINT('',#27988);
#8042=VERTEX_POINT('',#27992);
#8043=VERTEX_POINT('',#27996);
#8044=VERTEX_POINT('',#28000);
#8045=VERTEX_POINT('',#28004);
#8046=VERTEX_POINT('',#28008);
#8047=VERTEX_POINT('',#28012);
#8048=VERTEX_POINT('',#28016);
#8049=VERTEX_POINT('',#28018);
#8050=VERTEX_POINT('',#28022);
#8051=VERTEX_POINT('',#28026);
#8052=VERTEX_POINT('',#28030);
#8053=VERTEX_POINT('',#28034);
#8054=VERTEX_POINT('',#28038);
#8055=VERTEX_POINT('',#28042);
#8056=VERTEX_POINT('',#28048);
#8057=VERTEX_POINT('',#28052);
#8058=VERTEX_POINT('',#28056);
#8059=VERTEX_POINT('',#28060);
#8060=VERTEX_POINT('',#28064);
#8061=VERTEX_POINT('',#28068);
#8062=VERTEX_POINT('',#28072);
#8063=VERTEX_POINT('',#28076);
#8064=VERTEX_POINT('',#28080);
#8065=VERTEX_POINT('',#28084);
#8066=VERTEX_POINT('',#28088);
#8067=VERTEX_POINT('',#28095);
#8068=VERTEX_POINT('',#28096);
#8069=VERTEX_POINT('',#28098);
#8070=VERTEX_POINT('',#28100);
#8071=VERTEX_POINT('',#28104);
#8072=VERTEX_POINT('',#28106);
#8073=VERTEX_POINT('',#28110);
#8074=VERTEX_POINT('',#28112);
#8075=VERTEX_POINT('',#28116);
#8076=VERTEX_POINT('',#28118);
#8077=VERTEX_POINT('',#28122);
#8078=VERTEX_POINT('',#28124);
#8079=VERTEX_POINT('',#28128);
#8080=VERTEX_POINT('',#28130);
#8081=VERTEX_POINT('',#28134);
#8082=VERTEX_POINT('',#28136);
#8083=VERTEX_POINT('',#28140);
#8084=VERTEX_POINT('',#28141);
#8085=VERTEX_POINT('',#28143);
#8086=VERTEX_POINT('',#28145);
#8087=VERTEX_POINT('',#28147);
#8088=VERTEX_POINT('',#28149);
#8089=VERTEX_POINT('',#28151);
#8090=VERTEX_POINT('',#28153);
#8091=VERTEX_POINT('',#28155);
#8092=VERTEX_POINT('',#28157);
#8093=VERTEX_POINT('',#28159);
#8094=VERTEX_POINT('',#28161);
#8095=VERTEX_POINT('',#28163);
#8096=VERTEX_POINT('',#28165);
#8097=VERTEX_POINT('',#28167);
#8098=VERTEX_POINT('',#28169);
#8099=VERTEX_POINT('',#28171);
#8100=VERTEX_POINT('',#28173);
#8101=VERTEX_POINT('',#28175);
#8102=VERTEX_POINT('',#28177);
#8103=VERTEX_POINT('',#28179);
#8104=VERTEX_POINT('',#28181);
#8105=VERTEX_POINT('',#28183);
#8106=VERTEX_POINT('',#28185);
#8107=VERTEX_POINT('',#28187);
#8108=VERTEX_POINT('',#28189);
#8109=VERTEX_POINT('',#28191);
#8110=VERTEX_POINT('',#28193);
#8111=VERTEX_POINT('',#28196);
#8112=VERTEX_POINT('',#28198);
#8113=VERTEX_POINT('',#28200);
#8114=VERTEX_POINT('',#28202);
#8115=VERTEX_POINT('',#28204);
#8116=VERTEX_POINT('',#28206);
#8117=VERTEX_POINT('',#28208);
#8118=VERTEX_POINT('',#28210);
#8119=VERTEX_POINT('',#28214);
#8120=VERTEX_POINT('',#28216);
#8121=VERTEX_POINT('',#28220);
#8122=VERTEX_POINT('',#28224);
#8123=VERTEX_POINT('',#28228);
#8124=VERTEX_POINT('',#28231);
#8125=VERTEX_POINT('',#28233);
#8126=VERTEX_POINT('',#28236);
#8127=VERTEX_POINT('',#28240);
#8128=VERTEX_POINT('',#28244);
#8129=VERTEX_POINT('',#28246);
#8130=VERTEX_POINT('',#28248);
#8131=VERTEX_POINT('',#28250);
#8132=VERTEX_POINT('',#28252);
#8133=VERTEX_POINT('',#28254);
#8134=VERTEX_POINT('',#28256);
#8135=VERTEX_POINT('',#28258);
#8136=VERTEX_POINT('',#28261);
#8137=VERTEX_POINT('',#28263);
#8138=VERTEX_POINT('',#28265);
#8139=VERTEX_POINT('',#28267);
#8140=VERTEX_POINT('',#28269);
#8141=VERTEX_POINT('',#28271);
#8142=VERTEX_POINT('',#28273);
#8143=VERTEX_POINT('',#28275);
#8144=VERTEX_POINT('',#28277);
#8145=VERTEX_POINT('',#28279);
#8146=VERTEX_POINT('',#28281);
#8147=VERTEX_POINT('',#28283);
#8148=VERTEX_POINT('',#28285);
#8149=VERTEX_POINT('',#28287);
#8150=VERTEX_POINT('',#28289);
#8151=VERTEX_POINT('',#28291);
#8152=VERTEX_POINT('',#28293);
#8153=VERTEX_POINT('',#28295);
#8154=VERTEX_POINT('',#28297);
#8155=VERTEX_POINT('',#28299);
#8156=VERTEX_POINT('',#28301);
#8157=VERTEX_POINT('',#28313);
#8158=VERTEX_POINT('',#28315);
#8159=VERTEX_POINT('',#28319);
#8160=VERTEX_POINT('',#28323);
#8161=VERTEX_POINT('',#28327);
#8162=VERTEX_POINT('',#28331);
#8163=VERTEX_POINT('',#28385);
#8164=VERTEX_POINT('',#28386);
#8165=VERTEX_POINT('',#28388);
#8166=VERTEX_POINT('',#28390);
#8167=VERTEX_POINT('',#28394);
#8168=VERTEX_POINT('',#28396);
#8169=VERTEX_POINT('',#28400);
#8170=VERTEX_POINT('',#28402);
#8171=VERTEX_POINT('',#28406);
#8172=VERTEX_POINT('',#28408);
#8173=VERTEX_POINT('',#28412);
#8174=VERTEX_POINT('',#28414);
#8175=VERTEX_POINT('',#28418);
#8176=VERTEX_POINT('',#28420);
#8177=VERTEX_POINT('',#28424);
#8178=VERTEX_POINT('',#28426);
#8179=VERTEX_POINT('',#28430);
#8180=VERTEX_POINT('',#28432);
#8181=VERTEX_POINT('',#28436);
#8182=VERTEX_POINT('',#28437);
#8183=VERTEX_POINT('',#28439);
#8184=VERTEX_POINT('',#28441);
#8185=VERTEX_POINT('',#28445);
#8186=VERTEX_POINT('',#28447);
#8187=VERTEX_POINT('',#28451);
#8188=VERTEX_POINT('',#28453);
#8189=VERTEX_POINT('',#28457);
#8190=VERTEX_POINT('',#28459);
#8191=VERTEX_POINT('',#28463);
#8192=VERTEX_POINT('',#28465);
#8193=VERTEX_POINT('',#28469);
#8194=VERTEX_POINT('',#28471);
#8195=VERTEX_POINT('',#28475);
#8196=VERTEX_POINT('',#28477);
#8197=VERTEX_POINT('',#28481);
#8198=VERTEX_POINT('',#28483);
#8199=VERTEX_POINT('',#28487);
#8200=VERTEX_POINT('',#28488);
#8201=VERTEX_POINT('',#28492);
#8202=VERTEX_POINT('',#28494);
#8203=VERTEX_POINT('',#28496);
#8204=VERTEX_POINT('',#28498);
#8205=VERTEX_POINT('',#28500);
#8206=VERTEX_POINT('',#28502);
#8207=VERTEX_POINT('',#28504);
#8208=VERTEX_POINT('',#28506);
#8209=VERTEX_POINT('',#28508);
#8210=VERTEX_POINT('',#28510);
#8211=VERTEX_POINT('',#28512);
#8212=VERTEX_POINT('',#28514);
#8213=VERTEX_POINT('',#28516);
#8214=VERTEX_POINT('',#28518);
#8215=VERTEX_POINT('',#28520);
#8216=VERTEX_POINT('',#28522);
#8217=VERTEX_POINT('',#28528);
#8218=VERTEX_POINT('',#28532);
#8219=VERTEX_POINT('',#28536);
#8220=VERTEX_POINT('',#28540);
#8221=VERTEX_POINT('',#28544);
#8222=VERTEX_POINT('',#28548);
#8223=VERTEX_POINT('',#28552);
#8224=VERTEX_POINT('',#28556);
#8225=VERTEX_POINT('',#28560);
#8226=VERTEX_POINT('',#28564);
#8227=VERTEX_POINT('',#28568);
#8228=VERTEX_POINT('',#28572);
#8229=VERTEX_POINT('',#28576);
#8230=VERTEX_POINT('',#28580);
#8231=VERTEX_POINT('',#28584);
#8232=VERTEX_POINT('',#28588);
#8233=VERTEX_POINT('',#28592);
#8234=VERTEX_POINT('',#28596);
#10069=EDGE_CURVE('',#7995,#7996,#4245,.T.);
#10070=EDGE_CURVE('',#7997,#7995,#4246,.T.);
#10071=EDGE_CURVE('',#7998,#7997,#4247,.T.);
#10072=EDGE_CURVE('',#7999,#7998,#4248,.T.);
#10073=EDGE_CURVE('',#8000,#7999,#4249,.T.);
#10074=EDGE_CURVE('',#8001,#8000,#4250,.T.);
#10075=EDGE_CURVE('',#8002,#8001,#4251,.T.);
#10076=EDGE_CURVE('',#8003,#8002,#4252,.T.);
#10077=EDGE_CURVE('',#8004,#8003,#3497,.T.);
#10078=EDGE_CURVE('',#8005,#8004,#4253,.T.);
#10079=EDGE_CURVE('',#8006,#8005,#3498,.T.);
#10080=EDGE_CURVE('',#8007,#8006,#4254,.T.);
#10081=EDGE_CURVE('',#8008,#8007,#3499,.T.);
#10082=EDGE_CURVE('',#8009,#8008,#3500,.T.);
#10083=EDGE_CURVE('',#8010,#8009,#3501,.T.);
#10084=EDGE_CURVE('',#8011,#8010,#4255,.T.);
#10085=EDGE_CURVE('',#8012,#8011,#3502,.T.);
#10086=EDGE_CURVE('',#8013,#8012,#3503,.T.);
#10087=EDGE_CURVE('',#8014,#8013,#3504,.T.);
#10088=EDGE_CURVE('',#8015,#8014,#4256,.T.);
#10089=EDGE_CURVE('',#8016,#8015,#4257,.T.);
#10090=EDGE_CURVE('',#8017,#8016,#4258,.T.);
#10091=EDGE_CURVE('',#8018,#8017,#3505,.T.);
#10092=EDGE_CURVE('',#8019,#8018,#3506,.T.);
#10093=EDGE_CURVE('',#8020,#8019,#3507,.T.);
#10094=EDGE_CURVE('',#8021,#8020,#4259,.T.);
#10095=EDGE_CURVE('',#8022,#8021,#3508,.T.);
#10096=EDGE_CURVE('',#8023,#8022,#3509,.T.);
#10097=EDGE_CURVE('',#8024,#8023,#3510,.T.);
#10098=EDGE_CURVE('',#8025,#8024,#4260,.T.);
#10099=EDGE_CURVE('',#8026,#8025,#3511,.T.);
#10100=EDGE_CURVE('',#8027,#8026,#4261,.T.);
#10101=EDGE_CURVE('',#8028,#8027,#3512,.T.);
#10102=EDGE_CURVE('',#8029,#8028,#4262,.T.);
#10103=EDGE_CURVE('',#8030,#8029,#4263,.T.);
#10104=EDGE_CURVE('',#7996,#8030,#4264,.T.);
#10105=EDGE_CURVE('',#8014,#8031,#4265,.T.);
#10106=EDGE_CURVE('',#8032,#8031,#4266,.T.);
#10107=EDGE_CURVE('',#8015,#8032,#4267,.T.);
#10108=EDGE_CURVE('',#8013,#8033,#4268,.T.);
#10109=EDGE_CURVE('',#8031,#8033,#3513,.T.);
#10110=EDGE_CURVE('',#8012,#8034,#4269,.T.);
#10111=EDGE_CURVE('',#8033,#8034,#3514,.T.);
#10112=EDGE_CURVE('',#8011,#8035,#4270,.T.);
#10113=EDGE_CURVE('',#8034,#8035,#3515,.T.);
#10114=EDGE_CURVE('',#8010,#8036,#4271,.T.);
#10115=EDGE_CURVE('',#8035,#8036,#4272,.T.);
#10116=EDGE_CURVE('',#8009,#8037,#4273,.T.);
#10117=EDGE_CURVE('',#8036,#8037,#3516,.T.);
#10118=EDGE_CURVE('',#8008,#8038,#4274,.T.);
#10119=EDGE_CURVE('',#8037,#8038,#3517,.T.);
#10120=EDGE_CURVE('',#8007,#8039,#4275,.T.);
#10121=EDGE_CURVE('',#8038,#8039,#3518,.T.);
#10122=EDGE_CURVE('',#8006,#8040,#4276,.T.);
#10123=EDGE_CURVE('',#8039,#8040,#4277,.T.);
#10124=EDGE_CURVE('',#8005,#8041,#4278,.T.);
#10125=EDGE_CURVE('',#8040,#8041,#3519,.T.);
#10126=EDGE_CURVE('',#8004,#8042,#4279,.T.);
#10127=EDGE_CURVE('',#8041,#8042,#4280,.T.);
#10128=EDGE_CURVE('',#8003,#8043,#4281,.T.);
#10129=EDGE_CURVE('',#8042,#8043,#3520,.T.);
#10130=EDGE_CURVE('',#8002,#8044,#4282,.T.);
#10131=EDGE_CURVE('',#8043,#8044,#4283,.T.);
#10132=EDGE_CURVE('',#8001,#8045,#4284,.T.);
#10133=EDGE_CURVE('',#8044,#8045,#4285,.T.);
#10134=EDGE_CURVE('',#8000,#8046,#4286,.T.);
#10135=EDGE_CURVE('',#8045,#8046,#4287,.T.);
#10136=EDGE_CURVE('',#7999,#8047,#4288,.T.);
#10137=EDGE_CURVE('',#8046,#8047,#4289,.T.);
#10138=EDGE_CURVE('',#7996,#8048,#4290,.T.);
#10139=EDGE_CURVE('',#8049,#8048,#4291,.T.);
#10140=EDGE_CURVE('',#7995,#8049,#4292,.T.);
#10141=EDGE_CURVE('',#8030,#8050,#4293,.T.);
#10142=EDGE_CURVE('',#8048,#8050,#4294,.T.);
#10143=EDGE_CURVE('',#8029,#8051,#4295,.T.);
#10144=EDGE_CURVE('',#8050,#8051,#4296,.T.);
#10145=EDGE_CURVE('',#8028,#8052,#4297,.T.);
#10146=EDGE_CURVE('',#8051,#8052,#4298,.T.);
#10147=EDGE_CURVE('',#8027,#8053,#4299,.T.);
#10148=EDGE_CURVE('',#8052,#8053,#3521,.T.);
#10149=EDGE_CURVE('',#7998,#8054,#4300,.T.);
#10150=EDGE_CURVE('',#8047,#8054,#4301,.T.);
#10151=EDGE_CURVE('',#7997,#8055,#4302,.T.);
#10152=EDGE_CURVE('',#8054,#8055,#4303,.T.);
#10153=EDGE_CURVE('',#8055,#8049,#4304,.T.);
#10154=EDGE_CURVE('',#8056,#8026,#4305,.T.);
#10155=EDGE_CURVE('',#8053,#8056,#4306,.T.);
#10156=EDGE_CURVE('',#8057,#8032,#4307,.T.);
#10157=EDGE_CURVE('',#8016,#8057,#4308,.T.);
#10158=EDGE_CURVE('',#8058,#8057,#4309,.T.);
#10159=EDGE_CURVE('',#8017,#8058,#4310,.T.);
#10160=EDGE_CURVE('',#8059,#8058,#3522,.T.);
#10161=EDGE_CURVE('',#8018,#8059,#4311,.T.);
#10162=EDGE_CURVE('',#8060,#8059,#3523,.T.);
#10163=EDGE_CURVE('',#8019,#8060,#4312,.T.);
#10164=EDGE_CURVE('',#8061,#8060,#3524,.T.);
#10165=EDGE_CURVE('',#8020,#8061,#4313,.T.);
#10166=EDGE_CURVE('',#8062,#8061,#4314,.T.);
#10167=EDGE_CURVE('',#8021,#8062,#4315,.T.);
#10168=EDGE_CURVE('',#8063,#8062,#3525,.T.);
#10169=EDGE_CURVE('',#8022,#8063,#4316,.T.);
#10170=EDGE_CURVE('',#8064,#8063,#3526,.T.);
#10171=EDGE_CURVE('',#8023,#8064,#4317,.T.);
#10172=EDGE_CURVE('',#8065,#8064,#3527,.T.);
#10173=EDGE_CURVE('',#8024,#8065,#4318,.T.);
#10174=EDGE_CURVE('',#8066,#8065,#4319,.T.);
#10175=EDGE_CURVE('',#8025,#8066,#4320,.T.);
#10176=EDGE_CURVE('',#8056,#8066,#3528,.T.);
#10177=EDGE_CURVE('',#8067,#8068,#4321,.T.);
#10178=EDGE_CURVE('',#8069,#8067,#4322,.T.);
#10179=EDGE_CURVE('',#8069,#8070,#4323,.T.);
#10180=EDGE_CURVE('',#8070,#8068,#4324,.T.);
#10181=EDGE_CURVE('',#8068,#8071,#3529,.T.);
#10182=EDGE_CURVE('',#8070,#8072,#3530,.T.);
#10183=EDGE_CURVE('',#8072,#8071,#4325,.T.);
#10184=EDGE_CURVE('',#8071,#8073,#3531,.T.);
#10185=EDGE_CURVE('',#8072,#8074,#3532,.T.);
#10186=EDGE_CURVE('',#8074,#8073,#4326,.T.);
#10187=EDGE_CURVE('',#8073,#8075,#3533,.T.);
#10188=EDGE_CURVE('',#8074,#8076,#3534,.T.);
#10189=EDGE_CURVE('',#8076,#8075,#4327,.T.);
#10190=EDGE_CURVE('',#8075,#8077,#4328,.T.);
#10191=EDGE_CURVE('',#8076,#8078,#4329,.T.);
#10192=EDGE_CURVE('',#8078,#8077,#4330,.T.);
#10193=EDGE_CURVE('',#8077,#8079,#3535,.T.);
#10194=EDGE_CURVE('',#8078,#8080,#3536,.T.);
#10195=EDGE_CURVE('',#8080,#8079,#4331,.T.);
#10196=EDGE_CURVE('',#8079,#8081,#3537,.T.);
#10197=EDGE_CURVE('',#8080,#8082,#3538,.T.);
#10198=EDGE_CURVE('',#8082,#8081,#4332,.T.);
#10199=EDGE_CURVE('',#8083,#8084,#4333,.T.);
#10200=EDGE_CURVE('',#8084,#8085,#4334,.T.);
#10201=EDGE_CURVE('',#8085,#8086,#4335,.T.);
#10202=EDGE_CURVE('',#8086,#8087,#4336,.T.);
#10203=EDGE_CURVE('',#8087,#8088,#3539,.T.);
#10204=EDGE_CURVE('',#8088,#8089,#4337,.T.);
#10205=EDGE_CURVE('',#8090,#8089,#3540,.T.);
#10206=EDGE_CURVE('',#8091,#8090,#4338,.T.);
#10207=EDGE_CURVE('',#8092,#8091,#4339,.T.);
#10208=EDGE_CURVE('',#8093,#8092,#4340,.T.);
#10209=EDGE_CURVE('',#8094,#8093,#4341,.T.);
#10210=EDGE_CURVE('',#8094,#8095,#4342,.T.);
#10211=EDGE_CURVE('',#8095,#8096,#4343,.T.);
#10212=EDGE_CURVE('',#8096,#8097,#4344,.T.);
#10213=EDGE_CURVE('',#8097,#8098,#4345,.T.);
#10214=EDGE_CURVE('',#8098,#8099,#3541,.T.);
#10215=EDGE_CURVE('',#8099,#8100,#4346,.T.);
#10216=EDGE_CURVE('',#8100,#8101,#3542,.T.);
#10217=EDGE_CURVE('',#8101,#8102,#4347,.T.);
#10218=EDGE_CURVE('',#8102,#8103,#3543,.T.);
#10219=EDGE_CURVE('',#8103,#8104,#3544,.T.);
#10220=EDGE_CURVE('',#8104,#8105,#3545,.T.);
#10221=EDGE_CURVE('',#8105,#8106,#4348,.T.);
#10222=EDGE_CURVE('',#8106,#8107,#3546,.T.);
#10223=EDGE_CURVE('',#8107,#8108,#3547,.T.);
#10224=EDGE_CURVE('',#8108,#8109,#3548,.T.);
#10225=EDGE_CURVE('',#8109,#8110,#4349,.T.);
#10226=EDGE_CURVE('',#8110,#8067,#4350,.T.);
#10227=EDGE_CURVE('',#8081,#8111,#3549,.T.);
#10228=EDGE_CURVE('',#8111,#8112,#4351,.T.);
#10229=EDGE_CURVE('',#8112,#8113,#3550,.T.);
#10230=EDGE_CURVE('',#8113,#8114,#4352,.T.);
#10231=EDGE_CURVE('',#8114,#8115,#3551,.T.);
#10232=EDGE_CURVE('',#8115,#8116,#4353,.T.);
#10233=EDGE_CURVE('',#8116,#8117,#4354,.T.);
#10234=EDGE_CURVE('',#8117,#8118,#4355,.T.);
#10235=EDGE_CURVE('',#8118,#8083,#4356,.T.);
#10236=EDGE_CURVE('',#8119,#8084,#4357,.T.);
#10237=EDGE_CURVE('',#8120,#8083,#4358,.T.);
#10238=EDGE_CURVE('',#8119,#8120,#4359,.T.);
#10239=EDGE_CURVE('',#8121,#8085,#4360,.T.);
#10240=EDGE_CURVE('',#8121,#8119,#4361,.T.);
#10241=EDGE_CURVE('',#8122,#8086,#4362,.T.);
#10242=EDGE_CURVE('',#8122,#8121,#4363,.T.);
#10243=EDGE_CURVE('',#8123,#8087,#4364,.T.);
#10244=EDGE_CURVE('',#8123,#8122,#4365,.T.);
#10245=EDGE_CURVE('',#8124,#8124,#3552,.T.);
#10246=EDGE_CURVE('',#8125,#8125,#3553,.T.);
#10247=EDGE_CURVE('',#8126,#8088,#4366,.T.);
#10248=EDGE_CURVE('',#8126,#8123,#3554,.T.);
#10249=EDGE_CURVE('',#8126,#8127,#4367,.T.);
#10250=EDGE_CURVE('',#8127,#8089,#4368,.T.);
#10251=EDGE_CURVE('',#8128,#8120,#4369,.T.);
#10252=EDGE_CURVE('',#8129,#8128,#4370,.T.);
#10253=EDGE_CURVE('',#8130,#8129,#4371,.T.);
#10254=EDGE_CURVE('',#8131,#8130,#4372,.T.);
#10255=EDGE_CURVE('',#8132,#8131,#3555,.T.);
#10256=EDGE_CURVE('',#8133,#8132,#4373,.T.);
#10257=EDGE_CURVE('',#8134,#8133,#3556,.T.);
#10258=EDGE_CURVE('',#8135,#8134,#4374,.T.);
#10259=EDGE_CURVE('',#8082,#8135,#3557,.T.);
#10260=EDGE_CURVE('',#8136,#8069,#4375,.T.);
#10261=EDGE_CURVE('',#8137,#8136,#4376,.T.);
#10262=EDGE_CURVE('',#8138,#8137,#3558,.T.);
#10263=EDGE_CURVE('',#8139,#8138,#3559,.T.);
#10264=EDGE_CURVE('',#8140,#8139,#3560,.T.);
#10265=EDGE_CURVE('',#8141,#8140,#4377,.T.);
#10266=EDGE_CURVE('',#8142,#8141,#3561,.T.);
#10267=EDGE_CURVE('',#8143,#8142,#3562,.T.);
#10268=EDGE_CURVE('',#8144,#8143,#3563,.T.);
#10269=EDGE_CURVE('',#8145,#8144,#4378,.T.);
#10270=EDGE_CURVE('',#8146,#8145,#3564,.T.);
#10271=EDGE_CURVE('',#8147,#8146,#4379,.T.);
#10272=EDGE_CURVE('',#8148,#8147,#3565,.T.);
#10273=EDGE_CURVE('',#8149,#8148,#4380,.T.);
#10274=EDGE_CURVE('',#8150,#8149,#4381,.T.);
#10275=EDGE_CURVE('',#8151,#8150,#4382,.T.);
#10276=EDGE_CURVE('',#8152,#8151,#4383,.T.);
#10277=EDGE_CURVE('',#8153,#8152,#4384,.T.);
#10278=EDGE_CURVE('',#8154,#8153,#4385,.T.);
#10279=EDGE_CURVE('',#8155,#8154,#4386,.T.);
#10280=EDGE_CURVE('',#8156,#8155,#4387,.T.);
#10281=EDGE_CURVE('',#8127,#8156,#3566,.T.);
#10282=EDGE_CURVE('',#8153,#8093,#4388,.T.);
#10283=EDGE_CURVE('',#8094,#8152,#4389,.T.);
#10284=EDGE_CURVE('',#8154,#8092,#4390,.T.);
#10285=EDGE_CURVE('',#8155,#8091,#4391,.T.);
#10286=EDGE_CURVE('',#8156,#8090,#4392,.T.);
#10287=EDGE_CURVE('',#8157,#8157,#3567,.T.);
#10288=EDGE_CURVE('',#8158,#8158,#3568,.T.);
#10289=EDGE_CURVE('',#8125,#8159,#4393,.T.);
#10290=EDGE_CURVE('',#8159,#8159,#3569,.T.);
#10291=EDGE_CURVE('',#8158,#8160,#4394,.T.);
#10292=EDGE_CURVE('',#8160,#8160,#3570,.T.);
#10293=EDGE_CURVE('',#8124,#8161,#4395,.T.);
#10294=EDGE_CURVE('',#8161,#8161,#3571,.T.);
#10295=EDGE_CURVE('',#8157,#8162,#4396,.T.);
#10296=EDGE_CURVE('',#8162,#8162,#3572,.T.);
#10297=EDGE_CURVE('',#8128,#8118,#4397,.T.);
#10298=EDGE_CURVE('',#8129,#8117,#4398,.T.);
#10299=EDGE_CURVE('',#8130,#8116,#4399,.T.);
#10300=EDGE_CURVE('',#8131,#8115,#4400,.T.);
#10301=EDGE_CURVE('',#8132,#8114,#4401,.T.);
#10302=EDGE_CURVE('',#8133,#8113,#4402,.T.);
#10303=EDGE_CURVE('',#8134,#8112,#4403,.T.);
#10304=EDGE_CURVE('',#8135,#8111,#4404,.T.);
#10305=EDGE_CURVE('',#8151,#8095,#4405,.T.);
#10306=EDGE_CURVE('',#8150,#8096,#4406,.T.);
#10307=EDGE_CURVE('',#8149,#8097,#4407,.T.);
#10308=EDGE_CURVE('',#8148,#8098,#4408,.T.);
#10309=EDGE_CURVE('',#8147,#8099,#4409,.T.);
#10310=EDGE_CURVE('',#8100,#8146,#4410,.T.);
#10311=EDGE_CURVE('',#8145,#8101,#4411,.T.);
#10312=EDGE_CURVE('',#8144,#8102,#4412,.T.);
#10313=EDGE_CURVE('',#8143,#8103,#4413,.T.);
#10314=EDGE_CURVE('',#8142,#8104,#4414,.T.);
#10315=EDGE_CURVE('',#8141,#8105,#4415,.T.);
#10316=EDGE_CURVE('',#8140,#8106,#4416,.T.);
#10317=EDGE_CURVE('',#8139,#8107,#4417,.T.);
#10318=EDGE_CURVE('',#8138,#8108,#4418,.T.);
#10319=EDGE_CURVE('',#8137,#8109,#4419,.T.);
#10320=EDGE_CURVE('',#8136,#8110,#4420,.T.);
#10321=EDGE_CURVE('',#8163,#8164,#3573,.T.);
#10322=EDGE_CURVE('',#8165,#8163,#4421,.T.);
#10323=EDGE_CURVE('',#8166,#8165,#3574,.T.);
#10324=EDGE_CURVE('',#8166,#8164,#4422,.T.);
#10325=EDGE_CURVE('',#8164,#8167,#4423,.T.);
#10326=EDGE_CURVE('',#8168,#8166,#4424,.T.);
#10327=EDGE_CURVE('',#8168,#8167,#4425,.T.);
#10328=EDGE_CURVE('',#8167,#8169,#3575,.T.);
#10329=EDGE_CURVE('',#8170,#8168,#3576,.T.);
#10330=EDGE_CURVE('',#8170,#8169,#4426,.T.);
#10331=EDGE_CURVE('',#8169,#8171,#4427,.T.);
#10332=EDGE_CURVE('',#8172,#8170,#4428,.T.);
#10333=EDGE_CURVE('',#8172,#8171,#4429,.T.);
#10334=EDGE_CURVE('',#8171,#8173,#3577,.T.);
#10335=EDGE_CURVE('',#8174,#8172,#3578,.T.);
#10336=EDGE_CURVE('',#8174,#8173,#4430,.T.);
#10337=EDGE_CURVE('',#8173,#8175,#4431,.T.);
#10338=EDGE_CURVE('',#8176,#8174,#4432,.T.);
#10339=EDGE_CURVE('',#8176,#8175,#4433,.T.);
#10340=EDGE_CURVE('',#8175,#8177,#4434,.T.);
#10341=EDGE_CURVE('',#8178,#8176,#4435,.T.);
#10342=EDGE_CURVE('',#8178,#8177,#4436,.T.);
#10343=EDGE_CURVE('',#8177,#8179,#4437,.T.);
#10344=EDGE_CURVE('',#8180,#8178,#4438,.T.);
#10345=EDGE_CURVE('',#8180,#8179,#4439,.T.);
#10346=EDGE_CURVE('',#8181,#8182,#4440,.T.);
#10347=EDGE_CURVE('',#8183,#8182,#4441,.T.);
#10348=EDGE_CURVE('',#8184,#8183,#4442,.T.);
#10349=EDGE_CURVE('',#8184,#8181,#4443,.T.);
#10350=EDGE_CURVE('',#8185,#8181,#4444,.T.);
#10351=EDGE_CURVE('',#8186,#8184,#4445,.T.);
#10352=EDGE_CURVE('',#8186,#8185,#4446,.T.);
#10353=EDGE_CURVE('',#8187,#8185,#4447,.T.);
#10354=EDGE_CURVE('',#8188,#8186,#4448,.T.);
#10355=EDGE_CURVE('',#8188,#8187,#4449,.T.);
#10356=EDGE_CURVE('',#8187,#8189,#4450,.T.);
#10357=EDGE_CURVE('',#8190,#8188,#4451,.T.);
#10358=EDGE_CURVE('',#8190,#8189,#4452,.T.);
#10359=EDGE_CURVE('',#8189,#8191,#4453,.T.);
#10360=EDGE_CURVE('',#8192,#8190,#4454,.T.);
#10361=EDGE_CURVE('',#8192,#8191,#4455,.T.);
#10362=EDGE_CURVE('',#8191,#8193,#4456,.T.);
#10363=EDGE_CURVE('',#8194,#8192,#4457,.T.);
#10364=EDGE_CURVE('',#8194,#8193,#4458,.T.);
#10365=EDGE_CURVE('',#8193,#8195,#4459,.T.);
#10366=EDGE_CURVE('',#8196,#8194,#4460,.T.);
#10367=EDGE_CURVE('',#8196,#8195,#4461,.T.);
#10368=EDGE_CURVE('',#8195,#8197,#3579,.T.);
#10369=EDGE_CURVE('',#8198,#8196,#3580,.T.);
#10370=EDGE_CURVE('',#8198,#8197,#4462,.T.);
#10371=EDGE_CURVE('',#8199,#8200,#3581,.T.);
#10372=EDGE_CURVE('',#8200,#8198,#4463,.T.);
#10373=EDGE_CURVE('',#8183,#8180,#4464,.T.);
#10374=EDGE_CURVE('',#8165,#8201,#3582,.T.);
#10375=EDGE_CURVE('',#8201,#8202,#3583,.T.);
#10376=EDGE_CURVE('',#8202,#8203,#4465,.T.);
#10377=EDGE_CURVE('',#8203,#8204,#3584,.T.);
#10378=EDGE_CURVE('',#8204,#8205,#3585,.T.);
#10379=EDGE_CURVE('',#8205,#8206,#3586,.T.);
#10380=EDGE_CURVE('',#8206,#8207,#4466,.T.);
#10381=EDGE_CURVE('',#8207,#8208,#4467,.T.);
#10382=EDGE_CURVE('',#8208,#8209,#4468,.T.);
#10383=EDGE_CURVE('',#8209,#8210,#3587,.T.);
#10384=EDGE_CURVE('',#8210,#8211,#3588,.T.);
#10385=EDGE_CURVE('',#8211,#8212,#3589,.T.);
#10386=EDGE_CURVE('',#8212,#8213,#4469,.T.);
#10387=EDGE_CURVE('',#8213,#8214,#3590,.T.);
#10388=EDGE_CURVE('',#8214,#8215,#3591,.T.);
#10389=EDGE_CURVE('',#8215,#8216,#3592,.T.);
#10390=EDGE_CURVE('',#8216,#8199,#4470,.T.);
#10391=EDGE_CURVE('',#8179,#8182,#4471,.T.);
#10392=EDGE_CURVE('',#8197,#8217,#4472,.T.);
#10393=EDGE_CURVE('',#8217,#8200,#4473,.T.);
#10394=EDGE_CURVE('',#8217,#8218,#3593,.T.);
#10395=EDGE_CURVE('',#8199,#8218,#4474,.T.);
#10396=EDGE_CURVE('',#8218,#8219,#4475,.T.);
#10397=EDGE_CURVE('',#8216,#8219,#4476,.T.);
#10398=EDGE_CURVE('',#8219,#8220,#3594,.T.);
#10399=EDGE_CURVE('',#8215,#8220,#4477,.T.);
#10400=EDGE_CURVE('',#8220,#8221,#3595,.T.);
#10401=EDGE_CURVE('',#8214,#8221,#4478,.T.);
#10402=EDGE_CURVE('',#8221,#8222,#3596,.T.);
#10403=EDGE_CURVE('',#8213,#8222,#4479,.T.);
#10404=EDGE_CURVE('',#8222,#8223,#4480,.T.);
#10405=EDGE_CURVE('',#8212,#8223,#4481,.T.);
#10406=EDGE_CURVE('',#8223,#8224,#3597,.T.);
#10407=EDGE_CURVE('',#8211,#8224,#4482,.T.);
#10408=EDGE_CURVE('',#8224,#8225,#3598,.T.);
#10409=EDGE_CURVE('',#8210,#8225,#4483,.T.);
#10410=EDGE_CURVE('',#8225,#8226,#3599,.T.);
#10411=EDGE_CURVE('',#8209,#8226,#4484,.T.);
#10412=EDGE_CURVE('',#8226,#8227,#4485,.T.);
#10413=EDGE_CURVE('',#8208,#8227,#4486,.T.);
#10414=EDGE_CURVE('',#8227,#8228,#4487,.T.);
#10415=EDGE_CURVE('',#8207,#8228,#4488,.T.);
#10416=EDGE_CURVE('',#8228,#8229,#4489,.T.);
#10417=EDGE_CURVE('',#8206,#8229,#4490,.T.);
#10418=EDGE_CURVE('',#8229,#8230,#3600,.T.);
#10419=EDGE_CURVE('',#8205,#8230,#4491,.T.);
#10420=EDGE_CURVE('',#8230,#8231,#3601,.T.);
#10421=EDGE_CURVE('',#8204,#8231,#4492,.T.);
#10422=EDGE_CURVE('',#8231,#8232,#3602,.T.);
#10423=EDGE_CURVE('',#8203,#8232,#4493,.T.);
#10424=EDGE_CURVE('',#8232,#8233,#4494,.T.);
#10425=EDGE_CURVE('',#8202,#8233,#4495,.T.);
#10426=EDGE_CURVE('',#8233,#8234,#3603,.T.);
#10427=EDGE_CURVE('',#8201,#8234,#4496,.T.);
#10428=EDGE_CURVE('',#8234,#8163,#3604,.T.);
#13371=ORIENTED_EDGE('',*,*,#10069,.F.);
#13372=ORIENTED_EDGE('',*,*,#10070,.F.);
#13373=ORIENTED_EDGE('',*,*,#10071,.F.);
#13374=ORIENTED_EDGE('',*,*,#10072,.F.);
#13375=ORIENTED_EDGE('',*,*,#10073,.F.);
#13376=ORIENTED_EDGE('',*,*,#10074,.F.);
#13377=ORIENTED_EDGE('',*,*,#10075,.F.);
#13378=ORIENTED_EDGE('',*,*,#10076,.F.);
#13379=ORIENTED_EDGE('',*,*,#10077,.F.);
#13380=ORIENTED_EDGE('',*,*,#10078,.F.);
#13381=ORIENTED_EDGE('',*,*,#10079,.F.);
#13382=ORIENTED_EDGE('',*,*,#10080,.F.);
#13383=ORIENTED_EDGE('',*,*,#10081,.F.);
#13384=ORIENTED_EDGE('',*,*,#10082,.F.);
#13385=ORIENTED_EDGE('',*,*,#10083,.F.);
#13386=ORIENTED_EDGE('',*,*,#10084,.F.);
#13387=ORIENTED_EDGE('',*,*,#10085,.F.);
#13388=ORIENTED_EDGE('',*,*,#10086,.F.);
#13389=ORIENTED_EDGE('',*,*,#10087,.F.);
#13390=ORIENTED_EDGE('',*,*,#10088,.F.);
#13391=ORIENTED_EDGE('',*,*,#10089,.F.);
#13392=ORIENTED_EDGE('',*,*,#10090,.F.);
#13393=ORIENTED_EDGE('',*,*,#10091,.F.);
#13394=ORIENTED_EDGE('',*,*,#10092,.F.);
#13395=ORIENTED_EDGE('',*,*,#10093,.F.);
#13396=ORIENTED_EDGE('',*,*,#10094,.F.);
#13397=ORIENTED_EDGE('',*,*,#10095,.F.);
#13398=ORIENTED_EDGE('',*,*,#10096,.F.);
#13399=ORIENTED_EDGE('',*,*,#10097,.F.);
#13400=ORIENTED_EDGE('',*,*,#10098,.F.);
#13401=ORIENTED_EDGE('',*,*,#10099,.F.);
#13402=ORIENTED_EDGE('',*,*,#10100,.F.);
#13403=ORIENTED_EDGE('',*,*,#10101,.F.);
#13404=ORIENTED_EDGE('',*,*,#10102,.F.);
#13405=ORIENTED_EDGE('',*,*,#10103,.F.);
#13406=ORIENTED_EDGE('',*,*,#10104,.F.);
#13407=ORIENTED_EDGE('',*,*,#10088,.T.);
#13408=ORIENTED_EDGE('',*,*,#10105,.T.);
#13409=ORIENTED_EDGE('',*,*,#10106,.F.);
#13410=ORIENTED_EDGE('',*,*,#10107,.F.);
#13411=ORIENTED_EDGE('',*,*,#10087,.T.);
#13412=ORIENTED_EDGE('',*,*,#10108,.T.);
#13413=ORIENTED_EDGE('',*,*,#10109,.F.);
#13414=ORIENTED_EDGE('',*,*,#10105,.F.);
#13415=ORIENTED_EDGE('',*,*,#10086,.T.);
#13416=ORIENTED_EDGE('',*,*,#10110,.T.);
#13417=ORIENTED_EDGE('',*,*,#10111,.F.);
#13418=ORIENTED_EDGE('',*,*,#10108,.F.);
#13419=ORIENTED_EDGE('',*,*,#10085,.T.);
#13420=ORIENTED_EDGE('',*,*,#10112,.T.);
#13421=ORIENTED_EDGE('',*,*,#10113,.F.);
#13422=ORIENTED_EDGE('',*,*,#10110,.F.);
#13423=ORIENTED_EDGE('',*,*,#10084,.T.);
#13424=ORIENTED_EDGE('',*,*,#10114,.T.);
#13425=ORIENTED_EDGE('',*,*,#10115,.F.);
#13426=ORIENTED_EDGE('',*,*,#10112,.F.);
#13427=ORIENTED_EDGE('',*,*,#10083,.T.);
#13428=ORIENTED_EDGE('',*,*,#10116,.T.);
#13429=ORIENTED_EDGE('',*,*,#10117,.F.);
#13430=ORIENTED_EDGE('',*,*,#10114,.F.);
#13431=ORIENTED_EDGE('',*,*,#10082,.T.);
#13432=ORIENTED_EDGE('',*,*,#10118,.T.);
#13433=ORIENTED_EDGE('',*,*,#10119,.F.);
#13434=ORIENTED_EDGE('',*,*,#10116,.F.);
#13435=ORIENTED_EDGE('',*,*,#10081,.T.);
#13436=ORIENTED_EDGE('',*,*,#10120,.T.);
#13437=ORIENTED_EDGE('',*,*,#10121,.F.);
#13438=ORIENTED_EDGE('',*,*,#10118,.F.);
#13439=ORIENTED_EDGE('',*,*,#10080,.T.);
#13440=ORIENTED_EDGE('',*,*,#10122,.T.);
#13441=ORIENTED_EDGE('',*,*,#10123,.F.);
#13442=ORIENTED_EDGE('',*,*,#10120,.F.);
#13443=ORIENTED_EDGE('',*,*,#10079,.T.);
#13444=ORIENTED_EDGE('',*,*,#10124,.T.);
#13445=ORIENTED_EDGE('',*,*,#10125,.F.);
#13446=ORIENTED_EDGE('',*,*,#10122,.F.);
#13447=ORIENTED_EDGE('',*,*,#10078,.T.);
#13448=ORIENTED_EDGE('',*,*,#10126,.T.);
#13449=ORIENTED_EDGE('',*,*,#10127,.F.);
#13450=ORIENTED_EDGE('',*,*,#10124,.F.);
#13451=ORIENTED_EDGE('',*,*,#10077,.T.);
#13452=ORIENTED_EDGE('',*,*,#10128,.T.);
#13453=ORIENTED_EDGE('',*,*,#10129,.F.);
#13454=ORIENTED_EDGE('',*,*,#10126,.F.);
#13455=ORIENTED_EDGE('',*,*,#10076,.T.);
#13456=ORIENTED_EDGE('',*,*,#10130,.T.);
#13457=ORIENTED_EDGE('',*,*,#10131,.F.);
#13458=ORIENTED_EDGE('',*,*,#10128,.F.);
#13459=ORIENTED_EDGE('',*,*,#10075,.T.);
#13460=ORIENTED_EDGE('',*,*,#10132,.T.);
#13461=ORIENTED_EDGE('',*,*,#10133,.F.);
#13462=ORIENTED_EDGE('',*,*,#10130,.F.);
#13463=ORIENTED_EDGE('',*,*,#10074,.T.);
#13464=ORIENTED_EDGE('',*,*,#10134,.T.);
#13465=ORIENTED_EDGE('',*,*,#10135,.F.);
#13466=ORIENTED_EDGE('',*,*,#10132,.F.);
#13467=ORIENTED_EDGE('',*,*,#10073,.T.);
#13468=ORIENTED_EDGE('',*,*,#10136,.T.);
#13469=ORIENTED_EDGE('',*,*,#10137,.F.);
#13470=ORIENTED_EDGE('',*,*,#10134,.F.);
#13471=ORIENTED_EDGE('',*,*,#10069,.T.);
#13472=ORIENTED_EDGE('',*,*,#10138,.T.);
#13473=ORIENTED_EDGE('',*,*,#10139,.F.);
#13474=ORIENTED_EDGE('',*,*,#10140,.F.);
#13475=ORIENTED_EDGE('',*,*,#10104,.T.);
#13476=ORIENTED_EDGE('',*,*,#10141,.T.);
#13477=ORIENTED_EDGE('',*,*,#10142,.F.);
#13478=ORIENTED_EDGE('',*,*,#10138,.F.);
#13479=ORIENTED_EDGE('',*,*,#10103,.T.);
#13480=ORIENTED_EDGE('',*,*,#10143,.T.);
#13481=ORIENTED_EDGE('',*,*,#10144,.F.);
#13482=ORIENTED_EDGE('',*,*,#10141,.F.);
#13483=ORIENTED_EDGE('',*,*,#10102,.T.);
#13484=ORIENTED_EDGE('',*,*,#10145,.T.);
#13485=ORIENTED_EDGE('',*,*,#10146,.F.);
#13486=ORIENTED_EDGE('',*,*,#10143,.F.);
#13487=ORIENTED_EDGE('',*,*,#10101,.T.);
#13488=ORIENTED_EDGE('',*,*,#10147,.T.);
#13489=ORIENTED_EDGE('',*,*,#10148,.F.);
#13490=ORIENTED_EDGE('',*,*,#10145,.F.);
#13491=ORIENTED_EDGE('',*,*,#10072,.T.);
#13492=ORIENTED_EDGE('',*,*,#10149,.T.);
#13493=ORIENTED_EDGE('',*,*,#10150,.F.);
#13494=ORIENTED_EDGE('',*,*,#10136,.F.);
#13495=ORIENTED_EDGE('',*,*,#10071,.T.);
#13496=ORIENTED_EDGE('',*,*,#10151,.T.);
#13497=ORIENTED_EDGE('',*,*,#10152,.F.);
#13498=ORIENTED_EDGE('',*,*,#10149,.F.);
#13499=ORIENTED_EDGE('',*,*,#10070,.T.);
#13500=ORIENTED_EDGE('',*,*,#10140,.T.);
#13501=ORIENTED_EDGE('',*,*,#10153,.F.);
#13502=ORIENTED_EDGE('',*,*,#10151,.F.);
#13503=ORIENTED_EDGE('',*,*,#10100,.T.);
#13504=ORIENTED_EDGE('',*,*,#10154,.F.);
#13505=ORIENTED_EDGE('',*,*,#10155,.F.);
#13506=ORIENTED_EDGE('',*,*,#10147,.F.);
#13507=ORIENTED_EDGE('',*,*,#10089,.T.);
#13508=ORIENTED_EDGE('',*,*,#10107,.T.);
#13509=ORIENTED_EDGE('',*,*,#10156,.F.);
#13510=ORIENTED_EDGE('',*,*,#10157,.F.);
#13511=ORIENTED_EDGE('',*,*,#10090,.T.);
#13512=ORIENTED_EDGE('',*,*,#10157,.T.);
#13513=ORIENTED_EDGE('',*,*,#10158,.F.);
#13514=ORIENTED_EDGE('',*,*,#10159,.F.);
#13515=ORIENTED_EDGE('',*,*,#10091,.T.);
#13516=ORIENTED_EDGE('',*,*,#10159,.T.);
#13517=ORIENTED_EDGE('',*,*,#10160,.F.);
#13518=ORIENTED_EDGE('',*,*,#10161,.F.);
#13519=ORIENTED_EDGE('',*,*,#10092,.T.);
#13520=ORIENTED_EDGE('',*,*,#10161,.T.);
#13521=ORIENTED_EDGE('',*,*,#10162,.F.);
#13522=ORIENTED_EDGE('',*,*,#10163,.F.);
#13523=ORIENTED_EDGE('',*,*,#10093,.T.);
#13524=ORIENTED_EDGE('',*,*,#10163,.T.);
#13525=ORIENTED_EDGE('',*,*,#10164,.F.);
#13526=ORIENTED_EDGE('',*,*,#10165,.F.);
#13527=ORIENTED_EDGE('',*,*,#10094,.T.);
#13528=ORIENTED_EDGE('',*,*,#10165,.T.);
#13529=ORIENTED_EDGE('',*,*,#10166,.F.);
#13530=ORIENTED_EDGE('',*,*,#10167,.F.);
#13531=ORIENTED_EDGE('',*,*,#10095,.T.);
#13532=ORIENTED_EDGE('',*,*,#10167,.T.);
#13533=ORIENTED_EDGE('',*,*,#10168,.F.);
#13534=ORIENTED_EDGE('',*,*,#10169,.F.);
#13535=ORIENTED_EDGE('',*,*,#10096,.T.);
#13536=ORIENTED_EDGE('',*,*,#10169,.T.);
#13537=ORIENTED_EDGE('',*,*,#10170,.F.);
#13538=ORIENTED_EDGE('',*,*,#10171,.F.);
#13539=ORIENTED_EDGE('',*,*,#10097,.T.);
#13540=ORIENTED_EDGE('',*,*,#10171,.T.);
#13541=ORIENTED_EDGE('',*,*,#10172,.F.);
#13542=ORIENTED_EDGE('',*,*,#10173,.F.);
#13543=ORIENTED_EDGE('',*,*,#10098,.T.);
#13544=ORIENTED_EDGE('',*,*,#10173,.T.);
#13545=ORIENTED_EDGE('',*,*,#10174,.F.);
#13546=ORIENTED_EDGE('',*,*,#10175,.F.);
#13547=ORIENTED_EDGE('',*,*,#10099,.T.);
#13548=ORIENTED_EDGE('',*,*,#10175,.T.);
#13549=ORIENTED_EDGE('',*,*,#10176,.F.);
#13550=ORIENTED_EDGE('',*,*,#10154,.T.);
#13551=ORIENTED_EDGE('',*,*,#10176,.T.);
#13552=ORIENTED_EDGE('',*,*,#10174,.T.);
#13553=ORIENTED_EDGE('',*,*,#10172,.T.);
#13554=ORIENTED_EDGE('',*,*,#10170,.T.);
#13555=ORIENTED_EDGE('',*,*,#10168,.T.);
#13556=ORIENTED_EDGE('',*,*,#10166,.T.);
#13557=ORIENTED_EDGE('',*,*,#10164,.T.);
#13558=ORIENTED_EDGE('',*,*,#10162,.T.);
#13559=ORIENTED_EDGE('',*,*,#10160,.T.);
#13560=ORIENTED_EDGE('',*,*,#10158,.T.);
#13561=ORIENTED_EDGE('',*,*,#10156,.T.);
#13562=ORIENTED_EDGE('',*,*,#10106,.T.);
#13563=ORIENTED_EDGE('',*,*,#10109,.T.);
#13564=ORIENTED_EDGE('',*,*,#10111,.T.);
#13565=ORIENTED_EDGE('',*,*,#10113,.T.);
#13566=ORIENTED_EDGE('',*,*,#10115,.T.);
#13567=ORIENTED_EDGE('',*,*,#10117,.T.);
#13568=ORIENTED_EDGE('',*,*,#10119,.T.);
#13569=ORIENTED_EDGE('',*,*,#10121,.T.);
#13570=ORIENTED_EDGE('',*,*,#10123,.T.);
#13571=ORIENTED_EDGE('',*,*,#10125,.T.);
#13572=ORIENTED_EDGE('',*,*,#10127,.T.);
#13573=ORIENTED_EDGE('',*,*,#10129,.T.);
#13574=ORIENTED_EDGE('',*,*,#10131,.T.);
#13575=ORIENTED_EDGE('',*,*,#10133,.T.);
#13576=ORIENTED_EDGE('',*,*,#10135,.T.);
#13577=ORIENTED_EDGE('',*,*,#10137,.T.);
#13578=ORIENTED_EDGE('',*,*,#10150,.T.);
#13579=ORIENTED_EDGE('',*,*,#10152,.T.);
#13580=ORIENTED_EDGE('',*,*,#10153,.T.);
#13581=ORIENTED_EDGE('',*,*,#10139,.T.);
#13582=ORIENTED_EDGE('',*,*,#10142,.T.);
#13583=ORIENTED_EDGE('',*,*,#10144,.T.);
#13584=ORIENTED_EDGE('',*,*,#10146,.T.);
#13585=ORIENTED_EDGE('',*,*,#10148,.T.);
#13586=ORIENTED_EDGE('',*,*,#10155,.T.);
#13587=ORIENTED_EDGE('',*,*,#10177,.F.);
#13588=ORIENTED_EDGE('',*,*,#10178,.F.);
#13589=ORIENTED_EDGE('',*,*,#10179,.T.);
#13590=ORIENTED_EDGE('',*,*,#10180,.T.);
#13591=ORIENTED_EDGE('',*,*,#10181,.F.);
#13592=ORIENTED_EDGE('',*,*,#10180,.F.);
#13593=ORIENTED_EDGE('',*,*,#10182,.T.);
#13594=ORIENTED_EDGE('',*,*,#10183,.T.);
#13595=ORIENTED_EDGE('',*,*,#10184,.F.);
#13596=ORIENTED_EDGE('',*,*,#10183,.F.);
#13597=ORIENTED_EDGE('',*,*,#10185,.T.);
#13598=ORIENTED_EDGE('',*,*,#10186,.T.);
#13599=ORIENTED_EDGE('',*,*,#10187,.F.);
#13600=ORIENTED_EDGE('',*,*,#10186,.F.);
#13601=ORIENTED_EDGE('',*,*,#10188,.T.);
#13602=ORIENTED_EDGE('',*,*,#10189,.T.);
#13603=ORIENTED_EDGE('',*,*,#10190,.F.);
#13604=ORIENTED_EDGE('',*,*,#10189,.F.);
#13605=ORIENTED_EDGE('',*,*,#10191,.T.);
#13606=ORIENTED_EDGE('',*,*,#10192,.T.);
#13607=ORIENTED_EDGE('',*,*,#10193,.F.);
#13608=ORIENTED_EDGE('',*,*,#10192,.F.);
#13609=ORIENTED_EDGE('',*,*,#10194,.T.);
#13610=ORIENTED_EDGE('',*,*,#10195,.T.);
#13611=ORIENTED_EDGE('',*,*,#10196,.F.);
#13612=ORIENTED_EDGE('',*,*,#10195,.F.);
#13613=ORIENTED_EDGE('',*,*,#10197,.T.);
#13614=ORIENTED_EDGE('',*,*,#10198,.T.);
#13615=ORIENTED_EDGE('',*,*,#10199,.T.);
#13616=ORIENTED_EDGE('',*,*,#10200,.T.);
#13617=ORIENTED_EDGE('',*,*,#10201,.T.);
#13618=ORIENTED_EDGE('',*,*,#10202,.T.);
#13619=ORIENTED_EDGE('',*,*,#10203,.T.);
#13620=ORIENTED_EDGE('',*,*,#10204,.T.);
#13621=ORIENTED_EDGE('',*,*,#10205,.F.);
#13622=ORIENTED_EDGE('',*,*,#10206,.F.);
#13623=ORIENTED_EDGE('',*,*,#10207,.F.);
#13624=ORIENTED_EDGE('',*,*,#10208,.F.);
#13625=ORIENTED_EDGE('',*,*,#10209,.F.);
#13626=ORIENTED_EDGE('',*,*,#10210,.T.);
#13627=ORIENTED_EDGE('',*,*,#10211,.T.);
#13628=ORIENTED_EDGE('',*,*,#10212,.T.);
#13629=ORIENTED_EDGE('',*,*,#10213,.T.);
#13630=ORIENTED_EDGE('',*,*,#10214,.T.);
#13631=ORIENTED_EDGE('',*,*,#10215,.T.);
#13632=ORIENTED_EDGE('',*,*,#10216,.T.);
#13633=ORIENTED_EDGE('',*,*,#10217,.T.);
#13634=ORIENTED_EDGE('',*,*,#10218,.T.);
#13635=ORIENTED_EDGE('',*,*,#10219,.T.);
#13636=ORIENTED_EDGE('',*,*,#10220,.T.);
#13637=ORIENTED_EDGE('',*,*,#10221,.T.);
#13638=ORIENTED_EDGE('',*,*,#10222,.T.);
#13639=ORIENTED_EDGE('',*,*,#10223,.T.);
#13640=ORIENTED_EDGE('',*,*,#10224,.T.);
#13641=ORIENTED_EDGE('',*,*,#10225,.T.);
#13642=ORIENTED_EDGE('',*,*,#10226,.T.);
#13643=ORIENTED_EDGE('',*,*,#10177,.T.);
#13644=ORIENTED_EDGE('',*,*,#10181,.T.);
#13645=ORIENTED_EDGE('',*,*,#10184,.T.);
#13646=ORIENTED_EDGE('',*,*,#10187,.T.);
#13647=ORIENTED_EDGE('',*,*,#10190,.T.);
#13648=ORIENTED_EDGE('',*,*,#10193,.T.);
#13649=ORIENTED_EDGE('',*,*,#10196,.T.);
#13650=ORIENTED_EDGE('',*,*,#10227,.T.);
#13651=ORIENTED_EDGE('',*,*,#10228,.T.);
#13652=ORIENTED_EDGE('',*,*,#10229,.T.);
#13653=ORIENTED_EDGE('',*,*,#10230,.T.);
#13654=ORIENTED_EDGE('',*,*,#10231,.T.);
#13655=ORIENTED_EDGE('',*,*,#10232,.T.);
#13656=ORIENTED_EDGE('',*,*,#10233,.T.);
#13657=ORIENTED_EDGE('',*,*,#10234,.T.);
#13658=ORIENTED_EDGE('',*,*,#10235,.T.);
#13659=ORIENTED_EDGE('',*,*,#10236,.T.);
#13660=ORIENTED_EDGE('',*,*,#10199,.F.);
#13661=ORIENTED_EDGE('',*,*,#10237,.F.);
#13662=ORIENTED_EDGE('',*,*,#10238,.F.);
#13663=ORIENTED_EDGE('',*,*,#10239,.T.);
#13664=ORIENTED_EDGE('',*,*,#10200,.F.);
#13665=ORIENTED_EDGE('',*,*,#10236,.F.);
#13666=ORIENTED_EDGE('',*,*,#10240,.F.);
#13667=ORIENTED_EDGE('',*,*,#10241,.T.);
#13668=ORIENTED_EDGE('',*,*,#10201,.F.);
#13669=ORIENTED_EDGE('',*,*,#10239,.F.);
#13670=ORIENTED_EDGE('',*,*,#10242,.F.);
#13671=ORIENTED_EDGE('',*,*,#10243,.T.);
#13672=ORIENTED_EDGE('',*,*,#10202,.F.);
#13673=ORIENTED_EDGE('',*,*,#10241,.F.);
#13674=ORIENTED_EDGE('',*,*,#10244,.F.);
#13675=ORIENTED_EDGE('',*,*,#10245,.T.);
#13676=ORIENTED_EDGE('',*,*,#10246,.T.);
#13677=ORIENTED_EDGE('',*,*,#10247,.T.);
#13678=ORIENTED_EDGE('',*,*,#10203,.F.);
#13679=ORIENTED_EDGE('',*,*,#10243,.F.);
#13680=ORIENTED_EDGE('',*,*,#10248,.F.);
#13681=ORIENTED_EDGE('',*,*,#10204,.F.);
#13682=ORIENTED_EDGE('',*,*,#10247,.F.);
#13683=ORIENTED_EDGE('',*,*,#10249,.T.);
#13684=ORIENTED_EDGE('',*,*,#10250,.T.);
#13685=ORIENTED_EDGE('',*,*,#10238,.T.);
#13686=ORIENTED_EDGE('',*,*,#10251,.F.);
#13687=ORIENTED_EDGE('',*,*,#10252,.F.);
#13688=ORIENTED_EDGE('',*,*,#10253,.F.);
#13689=ORIENTED_EDGE('',*,*,#10254,.F.);
#13690=ORIENTED_EDGE('',*,*,#10255,.F.);
#13691=ORIENTED_EDGE('',*,*,#10256,.F.);
#13692=ORIENTED_EDGE('',*,*,#10257,.F.);
#13693=ORIENTED_EDGE('',*,*,#10258,.F.);
#13694=ORIENTED_EDGE('',*,*,#10259,.F.);
#13695=ORIENTED_EDGE('',*,*,#10197,.F.);
#13696=ORIENTED_EDGE('',*,*,#10194,.F.);
#13697=ORIENTED_EDGE('',*,*,#10191,.F.);
#13698=ORIENTED_EDGE('',*,*,#10188,.F.);
#13699=ORIENTED_EDGE('',*,*,#10185,.F.);
#13700=ORIENTED_EDGE('',*,*,#10182,.F.);
#13701=ORIENTED_EDGE('',*,*,#10179,.F.);
#13702=ORIENTED_EDGE('',*,*,#10260,.F.);
#13703=ORIENTED_EDGE('',*,*,#10261,.F.);
#13704=ORIENTED_EDGE('',*,*,#10262,.F.);
#13705=ORIENTED_EDGE('',*,*,#10263,.F.);
#13706=ORIENTED_EDGE('',*,*,#10264,.F.);
#13707=ORIENTED_EDGE('',*,*,#10265,.F.);
#13708=ORIENTED_EDGE('',*,*,#10266,.F.);
#13709=ORIENTED_EDGE('',*,*,#10267,.F.);
#13710=ORIENTED_EDGE('',*,*,#10268,.F.);
#13711=ORIENTED_EDGE('',*,*,#10269,.F.);
#13712=ORIENTED_EDGE('',*,*,#10270,.F.);
#13713=ORIENTED_EDGE('',*,*,#10271,.F.);
#13714=ORIENTED_EDGE('',*,*,#10272,.F.);
#13715=ORIENTED_EDGE('',*,*,#10273,.F.);
#13716=ORIENTED_EDGE('',*,*,#10274,.F.);
#13717=ORIENTED_EDGE('',*,*,#10275,.F.);
#13718=ORIENTED_EDGE('',*,*,#10276,.F.);
#13719=ORIENTED_EDGE('',*,*,#10277,.F.);
#13720=ORIENTED_EDGE('',*,*,#10278,.F.);
#13721=ORIENTED_EDGE('',*,*,#10279,.F.);
#13722=ORIENTED_EDGE('',*,*,#10280,.F.);
#13723=ORIENTED_EDGE('',*,*,#10281,.F.);
#13724=ORIENTED_EDGE('',*,*,#10249,.F.);
#13725=ORIENTED_EDGE('',*,*,#10248,.T.);
#13726=ORIENTED_EDGE('',*,*,#10244,.T.);
#13727=ORIENTED_EDGE('',*,*,#10242,.T.);
#13728=ORIENTED_EDGE('',*,*,#10240,.T.);
#13729=ORIENTED_EDGE('',*,*,#10282,.F.);
#13730=ORIENTED_EDGE('',*,*,#10277,.T.);
#13731=ORIENTED_EDGE('',*,*,#10283,.F.);
#13732=ORIENTED_EDGE('',*,*,#10209,.T.);
#13733=ORIENTED_EDGE('',*,*,#10284,.F.);
#13734=ORIENTED_EDGE('',*,*,#10278,.T.);
#13735=ORIENTED_EDGE('',*,*,#10282,.T.);
#13736=ORIENTED_EDGE('',*,*,#10208,.T.);
#13737=ORIENTED_EDGE('',*,*,#10285,.F.);
#13738=ORIENTED_EDGE('',*,*,#10279,.T.);
#13739=ORIENTED_EDGE('',*,*,#10284,.T.);
#13740=ORIENTED_EDGE('',*,*,#10207,.T.);
#13741=ORIENTED_EDGE('',*,*,#10286,.F.);
#13742=ORIENTED_EDGE('',*,*,#10280,.T.);
#13743=ORIENTED_EDGE('',*,*,#10285,.T.);
#13744=ORIENTED_EDGE('',*,*,#10206,.T.);
#13745=ORIENTED_EDGE('',*,*,#10287,.T.);
#13746=ORIENTED_EDGE('',*,*,#10288,.T.);
#13747=ORIENTED_EDGE('',*,*,#10250,.F.);
#13748=ORIENTED_EDGE('',*,*,#10281,.T.);
#13749=ORIENTED_EDGE('',*,*,#10286,.T.);
#13750=ORIENTED_EDGE('',*,*,#10205,.T.);
#13751=ORIENTED_EDGE('',*,*,#10246,.F.);
#13752=ORIENTED_EDGE('',*,*,#10289,.T.);
#13753=ORIENTED_EDGE('',*,*,#10290,.F.);
#13754=ORIENTED_EDGE('',*,*,#10289,.F.);
#13755=ORIENTED_EDGE('',*,*,#10288,.F.);
#13756=ORIENTED_EDGE('',*,*,#10291,.T.);
#13757=ORIENTED_EDGE('',*,*,#10292,.F.);
#13758=ORIENTED_EDGE('',*,*,#10291,.F.);
#13759=ORIENTED_EDGE('',*,*,#10245,.F.);
#13760=ORIENTED_EDGE('',*,*,#10293,.T.);
#13761=ORIENTED_EDGE('',*,*,#10294,.F.);
#13762=ORIENTED_EDGE('',*,*,#10293,.F.);
#13763=ORIENTED_EDGE('',*,*,#10287,.F.);
#13764=ORIENTED_EDGE('',*,*,#10295,.T.);
#13765=ORIENTED_EDGE('',*,*,#10296,.F.);
#13766=ORIENTED_EDGE('',*,*,#10295,.F.);
#13767=ORIENTED_EDGE('',*,*,#10235,.F.);
#13768=ORIENTED_EDGE('',*,*,#10297,.F.);
#13769=ORIENTED_EDGE('',*,*,#10251,.T.);
#13770=ORIENTED_EDGE('',*,*,#10237,.T.);
#13771=ORIENTED_EDGE('',*,*,#10234,.F.);
#13772=ORIENTED_EDGE('',*,*,#10298,.F.);
#13773=ORIENTED_EDGE('',*,*,#10252,.T.);
#13774=ORIENTED_EDGE('',*,*,#10297,.T.);
#13775=ORIENTED_EDGE('',*,*,#10233,.F.);
#13776=ORIENTED_EDGE('',*,*,#10299,.F.);
#13777=ORIENTED_EDGE('',*,*,#10253,.T.);
#13778=ORIENTED_EDGE('',*,*,#10298,.T.);
#13779=ORIENTED_EDGE('',*,*,#10290,.T.);
#13780=ORIENTED_EDGE('',*,*,#10294,.T.);
#13781=ORIENTED_EDGE('',*,*,#10232,.F.);
#13782=ORIENTED_EDGE('',*,*,#10300,.F.);
#13783=ORIENTED_EDGE('',*,*,#10254,.T.);
#13784=ORIENTED_EDGE('',*,*,#10299,.T.);
#13785=ORIENTED_EDGE('',*,*,#10231,.F.);
#13786=ORIENTED_EDGE('',*,*,#10301,.F.);
#13787=ORIENTED_EDGE('',*,*,#10255,.T.);
#13788=ORIENTED_EDGE('',*,*,#10300,.T.);
#13789=ORIENTED_EDGE('',*,*,#10230,.F.);
#13790=ORIENTED_EDGE('',*,*,#10302,.F.);
#13791=ORIENTED_EDGE('',*,*,#10256,.T.);
#13792=ORIENTED_EDGE('',*,*,#10301,.T.);
#13793=ORIENTED_EDGE('',*,*,#10229,.F.);
#13794=ORIENTED_EDGE('',*,*,#10303,.F.);
#13795=ORIENTED_EDGE('',*,*,#10257,.T.);
#13796=ORIENTED_EDGE('',*,*,#10302,.T.);
#13797=ORIENTED_EDGE('',*,*,#10228,.F.);
#13798=ORIENTED_EDGE('',*,*,#10304,.F.);
#13799=ORIENTED_EDGE('',*,*,#10258,.T.);
#13800=ORIENTED_EDGE('',*,*,#10303,.T.);
#13801=ORIENTED_EDGE('',*,*,#10227,.F.);
#13802=ORIENTED_EDGE('',*,*,#10198,.F.);
#13803=ORIENTED_EDGE('',*,*,#10259,.T.);
#13804=ORIENTED_EDGE('',*,*,#10304,.T.);
#13805=ORIENTED_EDGE('',*,*,#10210,.F.);
#13806=ORIENTED_EDGE('',*,*,#10283,.T.);
#13807=ORIENTED_EDGE('',*,*,#10276,.T.);
#13808=ORIENTED_EDGE('',*,*,#10305,.T.);
#13809=ORIENTED_EDGE('',*,*,#10211,.F.);
#13810=ORIENTED_EDGE('',*,*,#10305,.F.);
#13811=ORIENTED_EDGE('',*,*,#10275,.T.);
#13812=ORIENTED_EDGE('',*,*,#10306,.T.);
#13813=ORIENTED_EDGE('',*,*,#10212,.F.);
#13814=ORIENTED_EDGE('',*,*,#10306,.F.);
#13815=ORIENTED_EDGE('',*,*,#10274,.T.);
#13816=ORIENTED_EDGE('',*,*,#10307,.T.);
#13817=ORIENTED_EDGE('',*,*,#10296,.T.);
#13818=ORIENTED_EDGE('',*,*,#10292,.T.);
#13819=ORIENTED_EDGE('',*,*,#10213,.F.);
#13820=ORIENTED_EDGE('',*,*,#10307,.F.);
#13821=ORIENTED_EDGE('',*,*,#10273,.T.);
#13822=ORIENTED_EDGE('',*,*,#10308,.T.);
#13823=ORIENTED_EDGE('',*,*,#10214,.F.);
#13824=ORIENTED_EDGE('',*,*,#10308,.F.);
#13825=ORIENTED_EDGE('',*,*,#10272,.T.);
#13826=ORIENTED_EDGE('',*,*,#10309,.T.);
#13827=ORIENTED_EDGE('',*,*,#10215,.F.);
#13828=ORIENTED_EDGE('',*,*,#10309,.F.);
#13829=ORIENTED_EDGE('',*,*,#10271,.T.);
#13830=ORIENTED_EDGE('',*,*,#10310,.F.);
#13831=ORIENTED_EDGE('',*,*,#10216,.F.);
#13832=ORIENTED_EDGE('',*,*,#10310,.T.);
#13833=ORIENTED_EDGE('',*,*,#10270,.T.);
#13834=ORIENTED_EDGE('',*,*,#10311,.T.);
#13835=ORIENTED_EDGE('',*,*,#10217,.F.);
#13836=ORIENTED_EDGE('',*,*,#10311,.F.);
#13837=ORIENTED_EDGE('',*,*,#10269,.T.);
#13838=ORIENTED_EDGE('',*,*,#10312,.T.);
#13839=ORIENTED_EDGE('',*,*,#10218,.F.);
#13840=ORIENTED_EDGE('',*,*,#10312,.F.);
#13841=ORIENTED_EDGE('',*,*,#10268,.T.);
#13842=ORIENTED_EDGE('',*,*,#10313,.T.);
#13843=ORIENTED_EDGE('',*,*,#10219,.F.);
#13844=ORIENTED_EDGE('',*,*,#10313,.F.);
#13845=ORIENTED_EDGE('',*,*,#10267,.T.);
#13846=ORIENTED_EDGE('',*,*,#10314,.T.);
#13847=ORIENTED_EDGE('',*,*,#10220,.F.);
#13848=ORIENTED_EDGE('',*,*,#10314,.F.);
#13849=ORIENTED_EDGE('',*,*,#10266,.T.);
#13850=ORIENTED_EDGE('',*,*,#10315,.T.);
#13851=ORIENTED_EDGE('',*,*,#10221,.F.);
#13852=ORIENTED_EDGE('',*,*,#10315,.F.);
#13853=ORIENTED_EDGE('',*,*,#10265,.T.);
#13854=ORIENTED_EDGE('',*,*,#10316,.T.);
#13855=ORIENTED_EDGE('',*,*,#10222,.F.);
#13856=ORIENTED_EDGE('',*,*,#10316,.F.);
#13857=ORIENTED_EDGE('',*,*,#10264,.T.);
#13858=ORIENTED_EDGE('',*,*,#10317,.T.);
#13859=ORIENTED_EDGE('',*,*,#10223,.F.);
#13860=ORIENTED_EDGE('',*,*,#10317,.F.);
#13861=ORIENTED_EDGE('',*,*,#10263,.T.);
#13862=ORIENTED_EDGE('',*,*,#10318,.T.);
#13863=ORIENTED_EDGE('',*,*,#10224,.F.);
#13864=ORIENTED_EDGE('',*,*,#10318,.F.);
#13865=ORIENTED_EDGE('',*,*,#10262,.T.);
#13866=ORIENTED_EDGE('',*,*,#10319,.T.);
#13867=ORIENTED_EDGE('',*,*,#10225,.F.);
#13868=ORIENTED_EDGE('',*,*,#10319,.F.);
#13869=ORIENTED_EDGE('',*,*,#10261,.T.);
#13870=ORIENTED_EDGE('',*,*,#10320,.T.);
#13871=ORIENTED_EDGE('',*,*,#10226,.F.);
#13872=ORIENTED_EDGE('',*,*,#10320,.F.);
#13873=ORIENTED_EDGE('',*,*,#10260,.T.);
#13874=ORIENTED_EDGE('',*,*,#10178,.T.);
#13875=ORIENTED_EDGE('',*,*,#10321,.F.);
#13876=ORIENTED_EDGE('',*,*,#10322,.F.);
#13877=ORIENTED_EDGE('',*,*,#10323,.F.);
#13878=ORIENTED_EDGE('',*,*,#10324,.T.);
#13879=ORIENTED_EDGE('',*,*,#10325,.F.);
#13880=ORIENTED_EDGE('',*,*,#10324,.F.);
#13881=ORIENTED_EDGE('',*,*,#10326,.F.);
#13882=ORIENTED_EDGE('',*,*,#10327,.T.);
#13883=ORIENTED_EDGE('',*,*,#10328,.F.);
#13884=ORIENTED_EDGE('',*,*,#10327,.F.);
#13885=ORIENTED_EDGE('',*,*,#10329,.F.);
#13886=ORIENTED_EDGE('',*,*,#10330,.T.);
#13887=ORIENTED_EDGE('',*,*,#10331,.F.);
#13888=ORIENTED_EDGE('',*,*,#10330,.F.);
#13889=ORIENTED_EDGE('',*,*,#10332,.F.);
#13890=ORIENTED_EDGE('',*,*,#10333,.T.);
#13891=ORIENTED_EDGE('',*,*,#10334,.F.);
#13892=ORIENTED_EDGE('',*,*,#10333,.F.);
#13893=ORIENTED_EDGE('',*,*,#10335,.F.);
#13894=ORIENTED_EDGE('',*,*,#10336,.T.);
#13895=ORIENTED_EDGE('',*,*,#10337,.F.);
#13896=ORIENTED_EDGE('',*,*,#10336,.F.);
#13897=ORIENTED_EDGE('',*,*,#10338,.F.);
#13898=ORIENTED_EDGE('',*,*,#10339,.T.);
#13899=ORIENTED_EDGE('',*,*,#10340,.F.);
#13900=ORIENTED_EDGE('',*,*,#10339,.F.);
#13901=ORIENTED_EDGE('',*,*,#10341,.F.);
#13902=ORIENTED_EDGE('',*,*,#10342,.T.);
#13903=ORIENTED_EDGE('',*,*,#10343,.F.);
#13904=ORIENTED_EDGE('',*,*,#10342,.F.);
#13905=ORIENTED_EDGE('',*,*,#10344,.F.);
#13906=ORIENTED_EDGE('',*,*,#10345,.T.);
#13907=ORIENTED_EDGE('',*,*,#10346,.T.);
#13908=ORIENTED_EDGE('',*,*,#10347,.F.);
#13909=ORIENTED_EDGE('',*,*,#10348,.F.);
#13910=ORIENTED_EDGE('',*,*,#10349,.T.);
#13911=ORIENTED_EDGE('',*,*,#10350,.T.);
#13912=ORIENTED_EDGE('',*,*,#10349,.F.);
#13913=ORIENTED_EDGE('',*,*,#10351,.F.);
#13914=ORIENTED_EDGE('',*,*,#10352,.T.);
#13915=ORIENTED_EDGE('',*,*,#10353,.T.);
#13916=ORIENTED_EDGE('',*,*,#10352,.F.);
#13917=ORIENTED_EDGE('',*,*,#10354,.F.);
#13918=ORIENTED_EDGE('',*,*,#10355,.T.);
#13919=ORIENTED_EDGE('',*,*,#10356,.F.);
#13920=ORIENTED_EDGE('',*,*,#10355,.F.);
#13921=ORIENTED_EDGE('',*,*,#10357,.F.);
#13922=ORIENTED_EDGE('',*,*,#10358,.T.);
#13923=ORIENTED_EDGE('',*,*,#10359,.F.);
#13924=ORIENTED_EDGE('',*,*,#10358,.F.);
#13925=ORIENTED_EDGE('',*,*,#10360,.F.);
#13926=ORIENTED_EDGE('',*,*,#10361,.T.);
#13927=ORIENTED_EDGE('',*,*,#10362,.F.);
#13928=ORIENTED_EDGE('',*,*,#10361,.F.);
#13929=ORIENTED_EDGE('',*,*,#10363,.F.);
#13930=ORIENTED_EDGE('',*,*,#10364,.T.);
#13931=ORIENTED_EDGE('',*,*,#10365,.F.);
#13932=ORIENTED_EDGE('',*,*,#10364,.F.);
#13933=ORIENTED_EDGE('',*,*,#10366,.F.);
#13934=ORIENTED_EDGE('',*,*,#10367,.T.);
#13935=ORIENTED_EDGE('',*,*,#10368,.F.);
#13936=ORIENTED_EDGE('',*,*,#10367,.F.);
#13937=ORIENTED_EDGE('',*,*,#10369,.F.);
#13938=ORIENTED_EDGE('',*,*,#10370,.T.);
#13939=ORIENTED_EDGE('',*,*,#10371,.T.);
#13940=ORIENTED_EDGE('',*,*,#10372,.T.);
#13941=ORIENTED_EDGE('',*,*,#10369,.T.);
#13942=ORIENTED_EDGE('',*,*,#10366,.T.);
#13943=ORIENTED_EDGE('',*,*,#10363,.T.);
#13944=ORIENTED_EDGE('',*,*,#10360,.T.);
#13945=ORIENTED_EDGE('',*,*,#10357,.T.);
#13946=ORIENTED_EDGE('',*,*,#10354,.T.);
#13947=ORIENTED_EDGE('',*,*,#10351,.T.);
#13948=ORIENTED_EDGE('',*,*,#10348,.T.);
#13949=ORIENTED_EDGE('',*,*,#10373,.T.);
#13950=ORIENTED_EDGE('',*,*,#10344,.T.);
#13951=ORIENTED_EDGE('',*,*,#10341,.T.);
#13952=ORIENTED_EDGE('',*,*,#10338,.T.);
#13953=ORIENTED_EDGE('',*,*,#10335,.T.);
#13954=ORIENTED_EDGE('',*,*,#10332,.T.);
#13955=ORIENTED_EDGE('',*,*,#10329,.T.);
#13956=ORIENTED_EDGE('',*,*,#10326,.T.);
#13957=ORIENTED_EDGE('',*,*,#10323,.T.);
#13958=ORIENTED_EDGE('',*,*,#10374,.T.);
#13959=ORIENTED_EDGE('',*,*,#10375,.T.);
#13960=ORIENTED_EDGE('',*,*,#10376,.T.);
#13961=ORIENTED_EDGE('',*,*,#10377,.T.);
#13962=ORIENTED_EDGE('',*,*,#10378,.T.);
#13963=ORIENTED_EDGE('',*,*,#10379,.T.);
#13964=ORIENTED_EDGE('',*,*,#10380,.T.);
#13965=ORIENTED_EDGE('',*,*,#10381,.T.);
#13966=ORIENTED_EDGE('',*,*,#10382,.T.);
#13967=ORIENTED_EDGE('',*,*,#10383,.T.);
#13968=ORIENTED_EDGE('',*,*,#10384,.T.);
#13969=ORIENTED_EDGE('',*,*,#10385,.T.);
#13970=ORIENTED_EDGE('',*,*,#10386,.T.);
#13971=ORIENTED_EDGE('',*,*,#10387,.T.);
#13972=ORIENTED_EDGE('',*,*,#10388,.T.);
#13973=ORIENTED_EDGE('',*,*,#10389,.T.);
#13974=ORIENTED_EDGE('',*,*,#10390,.T.);
#13975=ORIENTED_EDGE('',*,*,#10391,.F.);
#13976=ORIENTED_EDGE('',*,*,#10345,.F.);
#13977=ORIENTED_EDGE('',*,*,#10373,.F.);
#13978=ORIENTED_EDGE('',*,*,#10347,.T.);
#13979=ORIENTED_EDGE('',*,*,#10392,.F.);
#13980=ORIENTED_EDGE('',*,*,#10370,.F.);
#13981=ORIENTED_EDGE('',*,*,#10372,.F.);
#13982=ORIENTED_EDGE('',*,*,#10393,.F.);
#13983=ORIENTED_EDGE('',*,*,#10394,.F.);
#13984=ORIENTED_EDGE('',*,*,#10393,.T.);
#13985=ORIENTED_EDGE('',*,*,#10371,.F.);
#13986=ORIENTED_EDGE('',*,*,#10395,.T.);
#13987=ORIENTED_EDGE('',*,*,#10396,.F.);
#13988=ORIENTED_EDGE('',*,*,#10395,.F.);
#13989=ORIENTED_EDGE('',*,*,#10390,.F.);
#13990=ORIENTED_EDGE('',*,*,#10397,.T.);
#13991=ORIENTED_EDGE('',*,*,#10398,.F.);
#13992=ORIENTED_EDGE('',*,*,#10397,.F.);
#13993=ORIENTED_EDGE('',*,*,#10389,.F.);
#13994=ORIENTED_EDGE('',*,*,#10399,.T.);
#13995=ORIENTED_EDGE('',*,*,#10400,.F.);
#13996=ORIENTED_EDGE('',*,*,#10399,.F.);
#13997=ORIENTED_EDGE('',*,*,#10388,.F.);
#13998=ORIENTED_EDGE('',*,*,#10401,.T.);
#13999=ORIENTED_EDGE('',*,*,#10402,.F.);
#14000=ORIENTED_EDGE('',*,*,#10401,.F.);
#14001=ORIENTED_EDGE('',*,*,#10387,.F.);
#14002=ORIENTED_EDGE('',*,*,#10403,.T.);
#14003=ORIENTED_EDGE('',*,*,#10404,.F.);
#14004=ORIENTED_EDGE('',*,*,#10403,.F.);
#14005=ORIENTED_EDGE('',*,*,#10386,.F.);
#14006=ORIENTED_EDGE('',*,*,#10405,.T.);
#14007=ORIENTED_EDGE('',*,*,#10406,.F.);
#14008=ORIENTED_EDGE('',*,*,#10405,.F.);
#14009=ORIENTED_EDGE('',*,*,#10385,.F.);
#14010=ORIENTED_EDGE('',*,*,#10407,.T.);
#14011=ORIENTED_EDGE('',*,*,#10408,.F.);
#14012=ORIENTED_EDGE('',*,*,#10407,.F.);
#14013=ORIENTED_EDGE('',*,*,#10384,.F.);
#14014=ORIENTED_EDGE('',*,*,#10409,.T.);
#14015=ORIENTED_EDGE('',*,*,#10410,.F.);
#14016=ORIENTED_EDGE('',*,*,#10409,.F.);
#14017=ORIENTED_EDGE('',*,*,#10383,.F.);
#14018=ORIENTED_EDGE('',*,*,#10411,.T.);
#14019=ORIENTED_EDGE('',*,*,#10412,.F.);
#14020=ORIENTED_EDGE('',*,*,#10411,.F.);
#14021=ORIENTED_EDGE('',*,*,#10382,.F.);
#14022=ORIENTED_EDGE('',*,*,#10413,.T.);
#14023=ORIENTED_EDGE('',*,*,#10414,.F.);
#14024=ORIENTED_EDGE('',*,*,#10413,.F.);
#14025=ORIENTED_EDGE('',*,*,#10381,.F.);
#14026=ORIENTED_EDGE('',*,*,#10415,.T.);
#14027=ORIENTED_EDGE('',*,*,#10416,.F.);
#14028=ORIENTED_EDGE('',*,*,#10415,.F.);
#14029=ORIENTED_EDGE('',*,*,#10380,.F.);
#14030=ORIENTED_EDGE('',*,*,#10417,.T.);
#14031=ORIENTED_EDGE('',*,*,#10418,.F.);
#14032=ORIENTED_EDGE('',*,*,#10417,.F.);
#14033=ORIENTED_EDGE('',*,*,#10379,.F.);
#14034=ORIENTED_EDGE('',*,*,#10419,.T.);
#14035=ORIENTED_EDGE('',*,*,#10420,.F.);
#14036=ORIENTED_EDGE('',*,*,#10419,.F.);
#14037=ORIENTED_EDGE('',*,*,#10378,.F.);
#14038=ORIENTED_EDGE('',*,*,#10421,.T.);
#14039=ORIENTED_EDGE('',*,*,#10422,.F.);
#14040=ORIENTED_EDGE('',*,*,#10421,.F.);
#14041=ORIENTED_EDGE('',*,*,#10377,.F.);
#14042=ORIENTED_EDGE('',*,*,#10423,.T.);
#14043=ORIENTED_EDGE('',*,*,#10424,.F.);
#14044=ORIENTED_EDGE('',*,*,#10423,.F.);
#14045=ORIENTED_EDGE('',*,*,#10376,.F.);
#14046=ORIENTED_EDGE('',*,*,#10425,.T.);
#14047=ORIENTED_EDGE('',*,*,#10426,.F.);
#14048=ORIENTED_EDGE('',*,*,#10425,.F.);
#14049=ORIENTED_EDGE('',*,*,#10375,.F.);
#14050=ORIENTED_EDGE('',*,*,#10427,.T.);
#14051=ORIENTED_EDGE('',*,*,#10428,.F.);
#14052=ORIENTED_EDGE('',*,*,#10427,.F.);
#14053=ORIENTED_EDGE('',*,*,#10374,.F.);
#14054=ORIENTED_EDGE('',*,*,#10322,.T.);
#14055=ORIENTED_EDGE('',*,*,#10392,.T.);
#14056=ORIENTED_EDGE('',*,*,#10394,.T.);
#14057=ORIENTED_EDGE('',*,*,#10396,.T.);
#14058=ORIENTED_EDGE('',*,*,#10398,.T.);
#14059=ORIENTED_EDGE('',*,*,#10400,.T.);
#14060=ORIENTED_EDGE('',*,*,#10402,.T.);
#14061=ORIENTED_EDGE('',*,*,#10404,.T.);
#14062=ORIENTED_EDGE('',*,*,#10406,.T.);
#14063=ORIENTED_EDGE('',*,*,#10408,.T.);
#14064=ORIENTED_EDGE('',*,*,#10410,.T.);
#14065=ORIENTED_EDGE('',*,*,#10412,.T.);
#14066=ORIENTED_EDGE('',*,*,#10414,.T.);
#14067=ORIENTED_EDGE('',*,*,#10416,.T.);
#14068=ORIENTED_EDGE('',*,*,#10418,.T.);
#14069=ORIENTED_EDGE('',*,*,#10420,.T.);
#14070=ORIENTED_EDGE('',*,*,#10422,.T.);
#14071=ORIENTED_EDGE('',*,*,#10424,.T.);
#14072=ORIENTED_EDGE('',*,*,#10426,.T.);
#14073=ORIENTED_EDGE('',*,*,#10428,.T.);
#14074=ORIENTED_EDGE('',*,*,#10321,.T.);
#14075=ORIENTED_EDGE('',*,*,#10325,.T.);
#14076=ORIENTED_EDGE('',*,*,#10328,.T.);
#14077=ORIENTED_EDGE('',*,*,#10331,.T.);
#14078=ORIENTED_EDGE('',*,*,#10334,.T.);
#14079=ORIENTED_EDGE('',*,*,#10337,.T.);
#14080=ORIENTED_EDGE('',*,*,#10340,.T.);
#14081=ORIENTED_EDGE('',*,*,#10343,.T.);
#14082=ORIENTED_EDGE('',*,*,#10391,.T.);
#14083=ORIENTED_EDGE('',*,*,#10346,.F.);
#14084=ORIENTED_EDGE('',*,*,#10350,.F.);
#14085=ORIENTED_EDGE('',*,*,#10353,.F.);
#14086=ORIENTED_EDGE('',*,*,#10356,.T.);
#14087=ORIENTED_EDGE('',*,*,#10359,.T.);
#14088=ORIENTED_EDGE('',*,*,#10362,.T.);
#14089=ORIENTED_EDGE('',*,*,#10365,.T.);
#14090=ORIENTED_EDGE('',*,*,#10368,.T.);
#18607=PLANE('',#20493);
#18608=PLANE('',#20510);
#18609=PLANE('',#20517);
#18610=PLANE('',#20524);
#18611=PLANE('',#20527);
#18612=PLANE('',#20530);
#18613=PLANE('',#20531);
#18614=PLANE('',#20532);
#18615=PLANE('',#20533);
#18616=PLANE('',#20534);
#18617=PLANE('',#20535);
#18618=PLANE('',#20536);
#18619=PLANE('',#20537);
#18620=PLANE('',#20540);
#18621=PLANE('',#20541);
#18622=PLANE('',#20542);
#18623=PLANE('',#20543);
#18624=PLANE('',#20544);
#18625=PLANE('',#20545);
#18626=PLANE('',#20552);
#18627=PLANE('',#20559);
#18628=PLANE('',#20562);
#18629=PLANE('',#20563);
#18630=PLANE('',#20573);
#18631=PLANE('',#20580);
#18632=PLANE('',#20594);
#18633=PLANE('',#20595);
#18634=PLANE('',#20596);
#18635=PLANE('',#20597);
#18636=PLANE('',#20602);
#18637=PLANE('',#20603);
#18638=PLANE('',#20616);
#18639=PLANE('',#20617);
#18640=PLANE('',#20618);
#18641=PLANE('',#20619);
#18642=PLANE('',#20631);
#18643=PLANE('',#20632);
#18644=PLANE('',#20633);
#18645=PLANE('',#20634);
#18646=PLANE('',#20636);
#18647=PLANE('',#20638);
#18648=PLANE('',#20640);
#18649=PLANE('',#20641);
#18650=PLANE('',#20642);
#18651=PLANE('',#20643);
#18652=PLANE('',#20645);
#18653=PLANE('',#20647);
#18654=PLANE('',#20651);
#18655=PLANE('',#20655);
#18656=PLANE('',#20656);
#18657=PLANE('',#20660);
#18658=PLANE('',#20664);
#18659=PLANE('',#20668);
#18660=PLANE('',#20669);
#18661=PLANE('',#20670);
#18662=PLANE('',#20671);
#18663=PLANE('',#20672);
#18664=PLANE('',#20673);
#18665=PLANE('',#20674);
#18666=PLANE('',#20675);
#18667=PLANE('',#20676);
#18668=PLANE('',#20677);
#18669=PLANE('',#20681);
#18670=PLANE('',#20694);
#18671=PLANE('',#20695);
#18672=PLANE('',#20698);
#18673=PLANE('',#20705);
#18674=PLANE('',#20712);
#18675=PLANE('',#20713);
#18676=PLANE('',#20714);
#18677=PLANE('',#20721);
#18678=PLANE('',#20726);
#19190=ADVANCED_FACE('',(#1333),#18607,.F.);
#19191=ADVANCED_FACE('',(#1334),#18608,.T.);
#19192=ADVANCED_FACE('',(#1335),#835,.F.);
#19193=ADVANCED_FACE('',(#1336),#836,.T.);
#19194=ADVANCED_FACE('',(#1337),#837,.F.);
#19195=ADVANCED_FACE('',(#1338),#18609,.T.);
#19196=ADVANCED_FACE('',(#1339),#838,.F.);
#19197=ADVANCED_FACE('',(#1340),#839,.T.);
#19198=ADVANCED_FACE('',(#1341),#840,.F.);
#19199=ADVANCED_FACE('',(#1342),#18610,.T.);
#19200=ADVANCED_FACE('',(#1343),#841,.T.);
#19201=ADVANCED_FACE('',(#1344),#18611,.T.);
#19202=ADVANCED_FACE('',(#1345),#842,.T.);
#19203=ADVANCED_FACE('',(#1346),#18612,.T.);
#19204=ADVANCED_FACE('',(#1347),#18613,.T.);
#19205=ADVANCED_FACE('',(#1348),#18614,.T.);
#19206=ADVANCED_FACE('',(#1349),#18615,.T.);
#19207=ADVANCED_FACE('',(#1350),#18616,.T.);
#19208=ADVANCED_FACE('',(#1351),#18617,.T.);
#19209=ADVANCED_FACE('',(#1352),#18618,.T.);
#19210=ADVANCED_FACE('',(#1353),#18619,.T.);
#19211=ADVANCED_FACE('',(#1354),#843,.T.);
#19212=ADVANCED_FACE('',(#1355),#18620,.T.);
#19213=ADVANCED_FACE('',(#1356),#18621,.T.);
#19214=ADVANCED_FACE('',(#1357),#18622,.T.);
#19215=ADVANCED_FACE('',(#1358),#18623,.T.);
#19216=ADVANCED_FACE('',(#1359),#18624,.T.);
#19217=ADVANCED_FACE('',(#1360),#18625,.T.);
#19218=ADVANCED_FACE('',(#1361),#844,.F.);
#19219=ADVANCED_FACE('',(#1362),#845,.T.);
#19220=ADVANCED_FACE('',(#1363),#846,.F.);
#19221=ADVANCED_FACE('',(#1364),#18626,.T.);
#19222=ADVANCED_FACE('',(#1365),#847,.F.);
#19223=ADVANCED_FACE('',(#1366),#848,.T.);
#19224=ADVANCED_FACE('',(#1367),#849,.F.);
#19225=ADVANCED_FACE('',(#1368),#18627,.T.);
#19226=ADVANCED_FACE('',(#1369),#850,.T.);
#19227=ADVANCED_FACE('',(#1370),#18628,.T.);
#19228=ADVANCED_FACE('',(#1371),#18629,.T.);
#19229=ADVANCED_FACE('',(#1372),#851,.F.);
#19230=ADVANCED_FACE('',(#1373),#852,.T.);
#19231=ADVANCED_FACE('',(#1374),#853,.F.);
#19232=ADVANCED_FACE('',(#1375),#18630,.T.);
#19233=ADVANCED_FACE('',(#1376),#854,.F.);
#19234=ADVANCED_FACE('',(#1377),#855,.T.);
#19235=ADVANCED_FACE('',(#1378),#18631,.T.);
#19236=ADVANCED_FACE('',(#1379),#18632,.T.);
#19237=ADVANCED_FACE('',(#1380),#18633,.T.);
#19238=ADVANCED_FACE('',(#1381),#18634,.T.);
#19239=ADVANCED_FACE('',(#1382,#643,#644),#18635,.T.);
#19240=ADVANCED_FACE('',(#1383),#856,.F.);
#19241=ADVANCED_FACE('',(#1384),#18636,.T.);
#19242=ADVANCED_FACE('',(#1385),#18637,.F.);
#19243=ADVANCED_FACE('',(#1386),#18638,.F.);
#19244=ADVANCED_FACE('',(#1387),#18639,.F.);
#19245=ADVANCED_FACE('',(#1388),#18640,.F.);
#19246=ADVANCED_FACE('',(#1389,#645,#646),#18641,.F.);
#19247=ADVANCED_FACE('',(#1390),#857,.F.);
#19248=ADVANCED_FACE('',(#1391),#858,.F.);
#19249=ADVANCED_FACE('',(#1392),#859,.F.);
#19250=ADVANCED_FACE('',(#1393),#860,.F.);
#19251=ADVANCED_FACE('',(#1394),#861,.F.);
#19252=ADVANCED_FACE('',(#1395),#18642,.T.);
#19253=ADVANCED_FACE('',(#1396),#18643,.T.);
#19254=ADVANCED_FACE('',(#1397,#647,#648),#18644,.T.);
#19255=ADVANCED_FACE('',(#1398),#18645,.T.);
#19256=ADVANCED_FACE('',(#1399),#862,.T.);
#19257=ADVANCED_FACE('',(#1400),#18646,.T.);
#19258=ADVANCED_FACE('',(#1401),#863,.T.);
#19259=ADVANCED_FACE('',(#1402),#18647,.T.);
#19260=ADVANCED_FACE('',(#1403),#864,.F.);
#19261=ADVANCED_FACE('',(#1404),#18648,.T.);
#19262=ADVANCED_FACE('',(#1405),#18649,.T.);
#19263=ADVANCED_FACE('',(#1406,#649,#650),#18650,.T.);
#19264=ADVANCED_FACE('',(#1407),#18651,.T.);
#19265=ADVANCED_FACE('',(#1408),#865,.T.);
#19266=ADVANCED_FACE('',(#1409),#18652,.T.);
#19267=ADVANCED_FACE('',(#1410),#866,.T.);
#19268=ADVANCED_FACE('',(#1411),#18653,.T.);
#19269=ADVANCED_FACE('',(#1412),#867,.F.);
#19270=ADVANCED_FACE('',(#1413),#868,.T.);
#19271=ADVANCED_FACE('',(#1414),#869,.F.);
#19272=ADVANCED_FACE('',(#1415),#18654,.T.);
#19273=ADVANCED_FACE('',(#1416),#870,.F.);
#19274=ADVANCED_FACE('',(#1417),#871,.T.);
#19275=ADVANCED_FACE('',(#1418),#872,.F.);
#19276=ADVANCED_FACE('',(#1419),#18655,.T.);
#19277=ADVANCED_FACE('',(#1420),#18656,.T.);
#19278=ADVANCED_FACE('',(#1421),#873,.F.);
#19279=ADVANCED_FACE('',(#1422),#18657,.T.);
#19280=ADVANCED_FACE('',(#1423),#874,.T.);
#19281=ADVANCED_FACE('',(#1424),#18658,.T.);
#19282=ADVANCED_FACE('',(#1425),#875,.T.);
#19283=ADVANCED_FACE('',(#1426),#18659,.T.);
#19284=ADVANCED_FACE('',(#1427),#18660,.T.);
#19285=ADVANCED_FACE('',(#1428),#18661,.T.);
#19286=ADVANCED_FACE('',(#1429),#18662,.T.);
#19287=ADVANCED_FACE('',(#1430),#18663,.T.);
#19288=ADVANCED_FACE('',(#1431),#18664,.T.);
#19289=ADVANCED_FACE('',(#1432),#18665,.T.);
#19290=ADVANCED_FACE('',(#1433),#18666,.T.);
#19291=ADVANCED_FACE('',(#1434),#18667,.T.);
#19292=ADVANCED_FACE('',(#1435),#18668,.T.);
#19293=ADVANCED_FACE('',(#1436),#876,.T.);
#19294=ADVANCED_FACE('',(#1437),#18669,.F.);
#19295=ADVANCED_FACE('',(#1438),#18670,.T.);
#19296=ADVANCED_FACE('',(#1439),#18671,.T.);
#19297=ADVANCED_FACE('',(#1440),#877,.T.);
#19298=ADVANCED_FACE('',(#1441),#18672,.T.);
#19299=ADVANCED_FACE('',(#1442),#878,.F.);
#19300=ADVANCED_FACE('',(#1443),#879,.T.);
#19301=ADVANCED_FACE('',(#1444),#880,.F.);
#19302=ADVANCED_FACE('',(#1445),#18673,.T.);
#19303=ADVANCED_FACE('',(#1446),#881,.F.);
#19304=ADVANCED_FACE('',(#1447),#882,.T.);
#19305=ADVANCED_FACE('',(#1448),#883,.F.);
#19306=ADVANCED_FACE('',(#1449),#18674,.T.);
#19307=ADVANCED_FACE('',(#1450),#18675,.T.);
#19308=ADVANCED_FACE('',(#1451),#18676,.T.);
#19309=ADVANCED_FACE('',(#1452),#884,.F.);
#19310=ADVANCED_FACE('',(#1453),#885,.T.);
#19311=ADVANCED_FACE('',(#1454),#886,.F.);
#19312=ADVANCED_FACE('',(#1455),#18677,.T.);
#19313=ADVANCED_FACE('',(#1456),#887,.F.);
#19314=ADVANCED_FACE('',(#1457),#888,.T.);
#19315=ADVANCED_FACE('',(#1458),#18678,.T.);
#20111=CLOSED_SHELL('',(#19190,#19191,#19192,#19193,#19194,#19195,#19196,
#19197,#19198,#19199,#19200,#19201,#19202,#19203,#19204,#19205,#19206,#19207,
#19208,#19209,#19210,#19211,#19212,#19213,#19214,#19215,#19216,#19217,#19218,
#19219,#19220,#19221,#19222,#19223,#19224,#19225,#19226,#19227));
#20112=CLOSED_SHELL('',(#19228,#19229,#19230,#19231,#19232,#19233,#19234,
#19235,#19236,#19237,#19238,#19239,#19240,#19241,#19242,#19243,#19244,#19245,
#19246,#19247,#19248,#19249,#19250,#19251,#19252,#19253,#19254,#19255,#19256,
#19257,#19258,#19259,#19260,#19261,#19262,#19263,#19264,#19265,#19266,#19267,
#19268,#19269,#19270,#19271,#19272,#19273,#19274,#19275,#19276,#19277));
#20113=CLOSED_SHELL('',(#19278,#19279,#19280,#19281,#19282,#19283,#19284,
#19285,#19286,#19287,#19288,#19289,#19290,#19291,#19292,#19293,#19294,#19295,
#19296,#19297,#19298,#19299,#19300,#19301,#19302,#19303,#19304,#19305,#19306,
#19307,#19308,#19309,#19310,#19311,#19312,#19313,#19314,#19315));
#20492=AXIS2_PLACEMENT_3D('',#27875,#22650,#22651);
#20493=AXIS2_PLACEMENT_3D('',#27876,#22652,#22653);
#20494=AXIS2_PLACEMENT_3D('',#27895,#22662,#22663);
#20495=AXIS2_PLACEMENT_3D('',#27899,#22665,#22666);
#20496=AXIS2_PLACEMENT_3D('',#27903,#22668,#22669);
#20497=AXIS2_PLACEMENT_3D('',#27905,#22670,#22671);
#20498=AXIS2_PLACEMENT_3D('',#27907,#22672,#22673);
#20499=AXIS2_PLACEMENT_3D('',#27911,#22675,#22676);
#20500=AXIS2_PLACEMENT_3D('',#27913,#22677,#22678);
#20501=AXIS2_PLACEMENT_3D('',#27915,#22679,#22680);
#20502=AXIS2_PLACEMENT_3D('',#27923,#22684,#22685);
#20503=AXIS2_PLACEMENT_3D('',#27925,#22686,#22687);
#20504=AXIS2_PLACEMENT_3D('',#27927,#22688,#22689);
#20505=AXIS2_PLACEMENT_3D('',#27931,#22691,#22692);
#20506=AXIS2_PLACEMENT_3D('',#27933,#22693,#22694);
#20507=AXIS2_PLACEMENT_3D('',#27935,#22695,#22696);
#20508=AXIS2_PLACEMENT_3D('',#27939,#22698,#22699);
#20509=AXIS2_PLACEMENT_3D('',#27943,#22701,#22702);
#20510=AXIS2_PLACEMENT_3D('',#27949,#22706,#22707);
#20511=AXIS2_PLACEMENT_3D('',#27955,#22711,#22712);
#20512=AXIS2_PLACEMENT_3D('',#27958,#22714,#22715);
#20513=AXIS2_PLACEMENT_3D('',#27959,#22716,#22717);
#20514=AXIS2_PLACEMENT_3D('',#27962,#22719,#22720);
#20515=AXIS2_PLACEMENT_3D('',#27963,#22721,#22722);
#20516=AXIS2_PLACEMENT_3D('',#27966,#22724,#22725);
#20517=AXIS2_PLACEMENT_3D('',#27967,#22726,#22727);
#20518=AXIS2_PLACEMENT_3D('',#27971,#22730,#22731);
#20519=AXIS2_PLACEMENT_3D('',#27974,#22733,#22734);
#20520=AXIS2_PLACEMENT_3D('',#27975,#22735,#22736);
#20521=AXIS2_PLACEMENT_3D('',#27978,#22738,#22739);
#20522=AXIS2_PLACEMENT_3D('',#27979,#22740,#22741);
#20523=AXIS2_PLACEMENT_3D('',#27982,#22743,#22744);
#20524=AXIS2_PLACEMENT_3D('',#27983,#22745,#22746);
#20525=AXIS2_PLACEMENT_3D('',#27987,#22749,#22750);
#20526=AXIS2_PLACEMENT_3D('',#27990,#22752,#22753);
#20527=AXIS2_PLACEMENT_3D('',#27991,#22754,#22755);
#20528=AXIS2_PLACEMENT_3D('',#27995,#22758,#22759);
#20529=AXIS2_PLACEMENT_3D('',#27998,#22761,#22762);
#20530=AXIS2_PLACEMENT_3D('',#27999,#22763,#22764);
#20531=AXIS2_PLACEMENT_3D('',#28003,#22767,#22768);
#20532=AXIS2_PLACEMENT_3D('',#28007,#22771,#22772);
#20533=AXIS2_PLACEMENT_3D('',#28011,#22775,#22776);
#20534=AXIS2_PLACEMENT_3D('',#28015,#22779,#22780);
#20535=AXIS2_PLACEMENT_3D('',#28021,#22784,#22785);
#20536=AXIS2_PLACEMENT_3D('',#28025,#22788,#22789);
#20537=AXIS2_PLACEMENT_3D('',#28029,#22792,#22793);
#20538=AXIS2_PLACEMENT_3D('',#28033,#22796,#22797);
#20539=AXIS2_PLACEMENT_3D('',#28036,#22799,#22800);
#20540=AXIS2_PLACEMENT_3D('',#28037,#22801,#22802);
#20541=AXIS2_PLACEMENT_3D('',#28041,#22805,#22806);
#20542=AXIS2_PLACEMENT_3D('',#28045,#22809,#22810);
#20543=AXIS2_PLACEMENT_3D('',#28047,#22812,#22813);
#20544=AXIS2_PLACEMENT_3D('',#28051,#22816,#22817);
#20545=AXIS2_PLACEMENT_3D('',#28055,#22820,#22821);
#20546=AXIS2_PLACEMENT_3D('',#28059,#22824,#22825);
#20547=AXIS2_PLACEMENT_3D('',#28061,#22826,#22827);
#20548=AXIS2_PLACEMENT_3D('',#28063,#22829,#22830);
#20549=AXIS2_PLACEMENT_3D('',#28065,#22831,#22832);
#20550=AXIS2_PLACEMENT_3D('',#28067,#22834,#22835);
#20551=AXIS2_PLACEMENT_3D('',#28069,#22836,#22837);
#20552=AXIS2_PLACEMENT_3D('',#28071,#22839,#22840);
#20553=AXIS2_PLACEMENT_3D('',#28075,#22843,#22844);
#20554=AXIS2_PLACEMENT_3D('',#28077,#22845,#22846);
#20555=AXIS2_PLACEMENT_3D('',#28079,#22848,#22849);
#20556=AXIS2_PLACEMENT_3D('',#28081,#22850,#22851);
#20557=AXIS2_PLACEMENT_3D('',#28083,#22853,#22854);
#20558=AXIS2_PLACEMENT_3D('',#28085,#22855,#22856);
#20559=AXIS2_PLACEMENT_3D('',#28087,#22858,#22859);
#20560=AXIS2_PLACEMENT_3D('',#28091,#22862,#22863);
#20561=AXIS2_PLACEMENT_3D('',#28092,#22864,#22865);
#20562=AXIS2_PLACEMENT_3D('',#28093,#22866,#22867);
#20563=AXIS2_PLACEMENT_3D('',#28094,#22868,#22869);
#20564=AXIS2_PLACEMENT_3D('',#28103,#22874,#22875);
#20565=AXIS2_PLACEMENT_3D('',#28105,#22876,#22877);
#20566=AXIS2_PLACEMENT_3D('',#28107,#22878,#22879);
#20567=AXIS2_PLACEMENT_3D('',#28109,#22881,#22882);
#20568=AXIS2_PLACEMENT_3D('',#28111,#22883,#22884);
#20569=AXIS2_PLACEMENT_3D('',#28113,#22885,#22886);
#20570=AXIS2_PLACEMENT_3D('',#28115,#22888,#22889);
#20571=AXIS2_PLACEMENT_3D('',#28117,#22890,#22891);
#20572=AXIS2_PLACEMENT_3D('',#28119,#22892,#22893);
#20573=AXIS2_PLACEMENT_3D('',#28121,#22895,#22896);
#20574=AXIS2_PLACEMENT_3D('',#28127,#22900,#22901);
#20575=AXIS2_PLACEMENT_3D('',#28129,#22902,#22903);
#20576=AXIS2_PLACEMENT_3D('',#28131,#22904,#22905);
#20577=AXIS2_PLACEMENT_3D('',#28133,#22907,#22908);
#20578=AXIS2_PLACEMENT_3D('',#28135,#22909,#22910);
#20579=AXIS2_PLACEMENT_3D('',#28137,#22911,#22912);
#20580=AXIS2_PLACEMENT_3D('',#28139,#22914,#22915);
#20581=AXIS2_PLACEMENT_3D('',#28150,#22920,#22921);
#20582=AXIS2_PLACEMENT_3D('',#28154,#22923,#22924);
#20583=AXIS2_PLACEMENT_3D('',#28172,#22933,#22934);
#20584=AXIS2_PLACEMENT_3D('',#28176,#22936,#22937);
#20585=AXIS2_PLACEMENT_3D('',#28180,#22939,#22940);
#20586=AXIS2_PLACEMENT_3D('',#28182,#22941,#22942);
#20587=AXIS2_PLACEMENT_3D('',#28184,#22943,#22944);
#20588=AXIS2_PLACEMENT_3D('',#28188,#22946,#22947);
#20589=AXIS2_PLACEMENT_3D('',#28190,#22948,#22949);
#20590=AXIS2_PLACEMENT_3D('',#28192,#22950,#22951);
#20591=AXIS2_PLACEMENT_3D('',#28197,#22954,#22955);
#20592=AXIS2_PLACEMENT_3D('',#28201,#22957,#22958);
#20593=AXIS2_PLACEMENT_3D('',#28205,#22960,#22961);
#20594=AXIS2_PLACEMENT_3D('',#28213,#22966,#22967);
#20595=AXIS2_PLACEMENT_3D('',#28219,#22971,#22972);
#20596=AXIS2_PLACEMENT_3D('',#28223,#22975,#22976);
#20597=AXIS2_PLACEMENT_3D('',#28227,#22979,#22980);
#20598=AXIS2_PLACEMENT_3D('',#28232,#22983,#22984);
#20599=AXIS2_PLACEMENT_3D('',#28234,#22985,#22986);
#20600=AXIS2_PLACEMENT_3D('',#28235,#22987,#22988);
#20601=AXIS2_PLACEMENT_3D('',#28238,#22990,#22991);
#20602=AXIS2_PLACEMENT_3D('',#28239,#22992,#22993);
#20603=AXIS2_PLACEMENT_3D('',#28243,#22996,#22997);
#20604=AXIS2_PLACEMENT_3D('',#28253,#23002,#23003);
#20605=AXIS2_PLACEMENT_3D('',#28257,#23005,#23006);
#20606=AXIS2_PLACEMENT_3D('',#28260,#23008,#23009);
#20607=AXIS2_PLACEMENT_3D('',#28266,#23012,#23013);
#20608=AXIS2_PLACEMENT_3D('',#28268,#23014,#23015);
#20609=AXIS2_PLACEMENT_3D('',#28270,#23016,#23017);
#20610=AXIS2_PLACEMENT_3D('',#28274,#23019,#23020);
#20611=AXIS2_PLACEMENT_3D('',#28276,#23021,#23022);
#20612=AXIS2_PLACEMENT_3D('',#28278,#23023,#23024);
#20613=AXIS2_PLACEMENT_3D('',#28282,#23026,#23027);
#20614=AXIS2_PLACEMENT_3D('',#28286,#23029,#23030);
#20615=AXIS2_PLACEMENT_3D('',#28303,#23039,#23040);
#20616=AXIS2_PLACEMENT_3D('',#28304,#23041,#23042);
#20617=AXIS2_PLACEMENT_3D('',#28307,#23045,#23046);
#20618=AXIS2_PLACEMENT_3D('',#28309,#23048,#23049);
#20619=AXIS2_PLACEMENT_3D('',#28311,#23051,#23052);
#20620=AXIS2_PLACEMENT_3D('',#28314,#23054,#23055);
#20621=AXIS2_PLACEMENT_3D('',#28316,#23056,#23057);
#20622=AXIS2_PLACEMENT_3D('',#28317,#23058,#23059);
#20623=AXIS2_PLACEMENT_3D('',#28318,#23060,#23061);
#20624=AXIS2_PLACEMENT_3D('',#28321,#23063,#23064);
#20625=AXIS2_PLACEMENT_3D('',#28322,#23065,#23066);
#20626=AXIS2_PLACEMENT_3D('',#28325,#23068,#23069);
#20627=AXIS2_PLACEMENT_3D('',#28326,#23070,#23071);
#20628=AXIS2_PLACEMENT_3D('',#28329,#23073,#23074);
#20629=AXIS2_PLACEMENT_3D('',#28330,#23075,#23076);
#20630=AXIS2_PLACEMENT_3D('',#28333,#23078,#23079);
#20631=AXIS2_PLACEMENT_3D('',#28334,#23080,#23081);
#20632=AXIS2_PLACEMENT_3D('',#28336,#23083,#23084);
#20633=AXIS2_PLACEMENT_3D('',#28338,#23086,#23087);
#20634=AXIS2_PLACEMENT_3D('',#28340,#23089,#23090);
#20635=AXIS2_PLACEMENT_3D('',#28342,#23092,#23093);
#20636=AXIS2_PLACEMENT_3D('',#28344,#23095,#23096);
#20637=AXIS2_PLACEMENT_3D('',#28346,#23098,#23099);
#20638=AXIS2_PLACEMENT_3D('',#28348,#23101,#23102);
#20639=AXIS2_PLACEMENT_3D('',#28350,#23104,#23105);
#20640=AXIS2_PLACEMENT_3D('',#28351,#23106,#23107);
#20641=AXIS2_PLACEMENT_3D('',#28353,#23109,#23110);
#20642=AXIS2_PLACEMENT_3D('',#28355,#23112,#23113);
#20643=AXIS2_PLACEMENT_3D('',#28357,#23115,#23116);
#20644=AXIS2_PLACEMENT_3D('',#28359,#23118,#23119);
#20645=AXIS2_PLACEMENT_3D('',#28361,#23121,#23122);
#20646=AXIS2_PLACEMENT_3D('',#28363,#23124,#23125);
#20647=AXIS2_PLACEMENT_3D('',#28365,#23127,#23128);
#20648=AXIS2_PLACEMENT_3D('',#28367,#23130,#23131);
#20649=AXIS2_PLACEMENT_3D('',#28369,#23133,#23134);
#20650=AXIS2_PLACEMENT_3D('',#28371,#23136,#23137);
#20651=AXIS2_PLACEMENT_3D('',#28373,#23139,#23140);
#20652=AXIS2_PLACEMENT_3D('',#28375,#23142,#23143);
#20653=AXIS2_PLACEMENT_3D('',#28377,#23145,#23146);
#20654=AXIS2_PLACEMENT_3D('',#28379,#23148,#23149);
#20655=AXIS2_PLACEMENT_3D('',#28381,#23151,#23152);
#20656=AXIS2_PLACEMENT_3D('',#28383,#23154,#23155);
#20657=AXIS2_PLACEMENT_3D('',#28384,#23156,#23157);
#20658=AXIS2_PLACEMENT_3D('',#28387,#23158,#23159);
#20659=AXIS2_PLACEMENT_3D('',#28391,#23161,#23162);
#20660=AXIS2_PLACEMENT_3D('',#28393,#23164,#23165);
#20661=AXIS2_PLACEMENT_3D('',#28399,#23169,#23170);
#20662=AXIS2_PLACEMENT_3D('',#28401,#23171,#23172);
#20663=AXIS2_PLACEMENT_3D('',#28403,#23173,#23174);
#20664=AXIS2_PLACEMENT_3D('',#28405,#23176,#23177);
#20665=AXIS2_PLACEMENT_3D('',#28411,#23181,#23182);
#20666=AXIS2_PLACEMENT_3D('',#28413,#23183,#23184);
#20667=AXIS2_PLACEMENT_3D('',#28415,#23185,#23186);
#20668=AXIS2_PLACEMENT_3D('',#28417,#23188,#23189);
#20669=AXIS2_PLACEMENT_3D('',#28423,#23193,#23194);
#20670=AXIS2_PLACEMENT_3D('',#28429,#23198,#23199);
#20671=AXIS2_PLACEMENT_3D('',#28435,#23203,#23204);
#20672=AXIS2_PLACEMENT_3D('',#28444,#23209,#23210);
#20673=AXIS2_PLACEMENT_3D('',#28450,#23214,#23215);
#20674=AXIS2_PLACEMENT_3D('',#28456,#23219,#23220);
#20675=AXIS2_PLACEMENT_3D('',#28462,#23224,#23225);
#20676=AXIS2_PLACEMENT_3D('',#28468,#23229,#23230);
#20677=AXIS2_PLACEMENT_3D('',#28474,#23234,#23235);
#20678=AXIS2_PLACEMENT_3D('',#28480,#23239,#23240);
#20679=AXIS2_PLACEMENT_3D('',#28482,#23241,#23242);
#20680=AXIS2_PLACEMENT_3D('',#28484,#23243,#23244);
#20681=AXIS2_PLACEMENT_3D('',#28486,#23246,#23247);
#20682=AXIS2_PLACEMENT_3D('',#28489,#23248,#23249);
#20683=AXIS2_PLACEMENT_3D('',#28493,#23252,#23253);
#20684=AXIS2_PLACEMENT_3D('',#28495,#23254,#23255);
#20685=AXIS2_PLACEMENT_3D('',#28499,#23257,#23258);
#20686=AXIS2_PLACEMENT_3D('',#28501,#23259,#23260);
#20687=AXIS2_PLACEMENT_3D('',#28503,#23261,#23262);
#20688=AXIS2_PLACEMENT_3D('',#28511,#23266,#23267);
#20689=AXIS2_PLACEMENT_3D('',#28513,#23268,#23269);
#20690=AXIS2_PLACEMENT_3D('',#28515,#23270,#23271);
#20691=AXIS2_PLACEMENT_3D('',#28519,#23273,#23274);
#20692=AXIS2_PLACEMENT_3D('',#28521,#23275,#23276);
#20693=AXIS2_PLACEMENT_3D('',#28523,#23277,#23278);
#20694=AXIS2_PLACEMENT_3D('',#28525,#23280,#23281);
#20695=AXIS2_PLACEMENT_3D('',#28527,#23283,#23284);
#20696=AXIS2_PLACEMENT_3D('',#28531,#23287,#23288);
#20697=AXIS2_PLACEMENT_3D('',#28533,#23289,#23290);
#20698=AXIS2_PLACEMENT_3D('',#28535,#23292,#23293);
#20699=AXIS2_PLACEMENT_3D('',#28539,#23296,#23297);
#20700=AXIS2_PLACEMENT_3D('',#28541,#23298,#23299);
#20701=AXIS2_PLACEMENT_3D('',#28543,#23301,#23302);
#20702=AXIS2_PLACEMENT_3D('',#28545,#23303,#23304);
#20703=AXIS2_PLACEMENT_3D('',#28547,#23306,#23307);
#20704=AXIS2_PLACEMENT_3D('',#28549,#23308,#23309);
#20705=AXIS2_PLACEMENT_3D('',#28551,#23311,#23312);
#20706=AXIS2_PLACEMENT_3D('',#28555,#23315,#23316);
#20707=AXIS2_PLACEMENT_3D('',#28557,#23317,#23318);
#20708=AXIS2_PLACEMENT_3D('',#28559,#23320,#23321);
#20709=AXIS2_PLACEMENT_3D('',#28561,#23322,#23323);
#20710=AXIS2_PLACEMENT_3D('',#28563,#23325,#23326);
#20711=AXIS2_PLACEMENT_3D('',#28565,#23327,#23328);
#20712=AXIS2_PLACEMENT_3D('',#28567,#23330,#23331);
#20713=AXIS2_PLACEMENT_3D('',#28571,#23334,#23335);
#20714=AXIS2_PLACEMENT_3D('',#28575,#23338,#23339);
#20715=AXIS2_PLACEMENT_3D('',#28579,#23342,#23343);
#20716=AXIS2_PLACEMENT_3D('',#28581,#23344,#23345);
#20717=AXIS2_PLACEMENT_3D('',#28583,#23347,#23348);
#20718=AXIS2_PLACEMENT_3D('',#28585,#23349,#23350);
#20719=AXIS2_PLACEMENT_3D('',#28587,#23352,#23353);
#20720=AXIS2_PLACEMENT_3D('',#28589,#23354,#23355);
#20721=AXIS2_PLACEMENT_3D('',#28591,#23357,#23358);
#20722=AXIS2_PLACEMENT_3D('',#28595,#23361,#23362);
#20723=AXIS2_PLACEMENT_3D('',#28597,#23363,#23364);
#20724=AXIS2_PLACEMENT_3D('',#28599,#23366,#23367);
#20725=AXIS2_PLACEMENT_3D('',#28600,#23368,#23369);
#20726=AXIS2_PLACEMENT_3D('',#28601,#23370,#23371);
#22650=DIRECTION('axis',(0.,0.,1.));
#22651=DIRECTION('refdir',(1.,0.,0.));
#22652=DIRECTION('center_axis',(0.,-1.,0.));
#22653=DIRECTION('ref_axis',(1.,0.,0.));
#22654=DIRECTION('',(-1.60844785188215E-15,0.,-1.));
#22655=DIRECTION('',(-0.707106781186551,0.,-0.707106781186544));
#22656=DIRECTION('',(-1.,0.,0.));
#22657=DIRECTION('',(-0.707106781186548,0.,0.707106781186548));
#22658=DIRECTION('',(0.,0.,1.));
#22659=DIRECTION('',(0.707106781186549,0.,0.707106781186546));
#22660=DIRECTION('',(1.,0.,0.));
#22661=DIRECTION('',(0.70472729891367,0.,-0.709478283082607));
#22662=DIRECTION('center_axis',(0.,-1.,0.));
#22663=DIRECTION('ref_axis',(-1.,0.,7.19001577852613E-14));
#22664=DIRECTION('',(1.18143967662125E-14,0.,-1.));
#22665=DIRECTION('center_axis',(0.,-1.,0.));
#22666=DIRECTION('ref_axis',(-0.711979844231317,0.,0.702199901316106));
#22667=DIRECTION('',(-0.702199901316085,0.,-0.711979844231338));
#22668=DIRECTION('center_axis',(0.,1.,0.));
#22669=DIRECTION('ref_axis',(0.711979844231347,0.,-0.702199901316076));
#22670=DIRECTION('center_axis',(0.,-1.,0.));
#22671=DIRECTION('ref_axis',(-0.245760053518557,0.,0.969330694909924));
#22672=DIRECTION('center_axis',(0.,1.,0.));
#22673=DIRECTION('ref_axis',(0.245760053518526,0.,-0.969330694909932));
#22674=DIRECTION('',(0.,0.,-1.));
#22675=DIRECTION('center_axis',(0.,1.,0.));
#22676=DIRECTION('ref_axis',(1.,0.,0.));
#22677=DIRECTION('center_axis',(0.,-1.,0.));
#22678=DIRECTION('ref_axis',(-0.963381374692976,0.,-0.268134904282661));
#22679=DIRECTION('center_axis',(0.,1.,0.));
#22680=DIRECTION('ref_axis',(0.963381374692962,0.,0.26813490428271));
#22681=DIRECTION('',(0.703465658964231,0.,-0.710729249896204));
#22682=DIRECTION('',(1.,0.,-6.14369354430926E-16));
#22683=DIRECTION('',(0.703465658964212,0.,0.710729249896223));
#22684=DIRECTION('center_axis',(0.,1.,0.));
#22685=DIRECTION('ref_axis',(-0.710729249896308,0.,0.703465658964126));
#22686=DIRECTION('center_axis',(0.,-1.,0.));
#22687=DIRECTION('ref_axis',(0.295138112194494,0.,-0.955454601082788));
#22688=DIRECTION('center_axis',(0.,1.,0.));
#22689=DIRECTION('ref_axis',(-0.295138112194515,0.,0.955454601082782));
#22690=DIRECTION('',(1.93287220490857E-14,0.,1.));
#22691=DIRECTION('center_axis',(0.,1.,0.));
#22692=DIRECTION('ref_axis',(-1.,0.,1.48029736616691E-14));
#22693=DIRECTION('center_axis',(0.,-1.,0.));
#22694=DIRECTION('ref_axis',(0.951733868867033,0.,0.306924490471823));
#22695=DIRECTION('center_axis',(0.,1.,0.));
#22696=DIRECTION('ref_axis',(-0.951733868867053,0.,-0.306924490471762));
#22697=DIRECTION('',(-0.702199901316075,0.,0.711979844231348));
#22698=DIRECTION('center_axis',(0.,-1.,0.));
#22699=DIRECTION('ref_axis',(1.,0.,0.));
#22700=DIRECTION('',(0.,0.,1.));
#22701=DIRECTION('center_axis',(0.,-1.,0.));
#22702=DIRECTION('ref_axis',(0.709478283082593,0.,-0.704727298913683));
#22703=DIRECTION('',(0.704727298913668,0.,0.709478283082608));
#22704=DIRECTION('',(1.,0.,-1.55356845212375E-15));
#22705=DIRECTION('',(0.707106781186549,0.,-0.707106781186546));
#22706=DIRECTION('center_axis',(-0.710729249896204,0.,-0.703465658964231));
#22707=DIRECTION('ref_axis',(0.703465658964231,0.,-0.710729249896204));
#22708=DIRECTION('',(0.,-1.,0.));
#22709=DIRECTION('',(0.703465658964231,0.,-0.710729249896204));
#22710=DIRECTION('',(0.,-1.,0.));
#22711=DIRECTION('center_axis',(0.,-1.,0.));
#22712=DIRECTION('ref_axis',(0.963381374692962,0.,0.26813490428271));
#22713=DIRECTION('',(0.,-1.,0.));
#22714=DIRECTION('center_axis',(0.,1.,0.));
#22715=DIRECTION('ref_axis',(0.963381374692962,0.,0.26813490428271));
#22716=DIRECTION('center_axis',(0.,-1.,0.));
#22717=DIRECTION('ref_axis',(-0.963381374692976,0.,-0.268134904282661));
#22718=DIRECTION('',(0.,-1.,0.));
#22719=DIRECTION('center_axis',(0.,-1.,0.));
#22720=DIRECTION('ref_axis',(-0.963381374692976,0.,-0.268134904282661));
#22721=DIRECTION('center_axis',(0.,-1.,0.));
#22722=DIRECTION('ref_axis',(1.,0.,0.));
#22723=DIRECTION('',(0.,-1.,0.));
#22724=DIRECTION('center_axis',(0.,1.,0.));
#22725=DIRECTION('ref_axis',(1.,0.,0.));
#22726=DIRECTION('center_axis',(-1.,0.,0.));
#22727=DIRECTION('ref_axis',(0.,0.,-1.));
#22728=DIRECTION('',(0.,-1.,0.));
#22729=DIRECTION('',(0.,0.,-1.));
#22730=DIRECTION('center_axis',(0.,-1.,0.));
#22731=DIRECTION('ref_axis',(0.245760053518526,0.,-0.969330694909932));
#22732=DIRECTION('',(0.,-1.,0.));
#22733=DIRECTION('center_axis',(0.,1.,0.));
#22734=DIRECTION('ref_axis',(0.245760053518526,0.,-0.969330694909932));
#22735=DIRECTION('center_axis',(0.,-1.,0.));
#22736=DIRECTION('ref_axis',(-0.245760053518557,0.,0.969330694909924));
#22737=DIRECTION('',(0.,-1.,0.));
#22738=DIRECTION('center_axis',(0.,-1.,0.));
#22739=DIRECTION('ref_axis',(-0.245760053518557,0.,0.969330694909924));
#22740=DIRECTION('center_axis',(0.,-1.,0.));
#22741=DIRECTION('ref_axis',(0.711979844231347,0.,-0.702199901316076));
#22742=DIRECTION('',(0.,-1.,0.));
#22743=DIRECTION('center_axis',(0.,1.,0.));
#22744=DIRECTION('ref_axis',(0.711979844231347,0.,-0.702199901316076));
#22745=DIRECTION('center_axis',(-0.711979844231338,0.,0.702199901316085));
#22746=DIRECTION('ref_axis',(-0.702199901316085,0.,-0.711979844231338));
#22747=DIRECTION('',(0.,-1.,0.));
#22748=DIRECTION('',(-0.702199901316085,0.,-0.711979844231338));
#22749=DIRECTION('center_axis',(0.,-1.,0.));
#22750=DIRECTION('ref_axis',(-0.711979844231317,0.,0.702199901316106));
#22751=DIRECTION('',(0.,-1.,0.));
#22752=DIRECTION('center_axis',(0.,-1.,0.));
#22753=DIRECTION('ref_axis',(-0.711979844231317,0.,0.702199901316106));
#22754=DIRECTION('center_axis',(-1.,0.,-1.18143967662125E-14));
#22755=DIRECTION('ref_axis',(1.18143967662125E-14,0.,-1.));
#22756=DIRECTION('',(0.,-1.,0.));
#22757=DIRECTION('',(1.18143967662125E-14,0.,-1.));
#22758=DIRECTION('center_axis',(0.,-1.,0.));
#22759=DIRECTION('ref_axis',(-1.,0.,7.19001577852613E-14));
#22760=DIRECTION('',(0.,-1.,0.));
#22761=DIRECTION('center_axis',(0.,-1.,0.));
#22762=DIRECTION('ref_axis',(-1.,0.,7.19001577852613E-14));
#22763=DIRECTION('center_axis',(-0.709478283082607,0.,-0.70472729891367));
#22764=DIRECTION('ref_axis',(0.70472729891367,0.,-0.709478283082607));
#22765=DIRECTION('',(0.,-1.,0.));
#22766=DIRECTION('',(0.70472729891367,0.,-0.709478283082607));
#22767=DIRECTION('center_axis',(0.,0.,-1.));
#22768=DIRECTION('ref_axis',(1.,0.,0.));
#22769=DIRECTION('',(0.,-1.,0.));
#22770=DIRECTION('',(1.,0.,0.));
#22771=DIRECTION('center_axis',(0.707106781186546,0.,-0.707106781186549));
#22772=DIRECTION('ref_axis',(0.707106781186549,0.,0.707106781186546));
#22773=DIRECTION('',(0.,-1.,0.));
#22774=DIRECTION('',(0.707106781186549,0.,0.707106781186546));
#22775=DIRECTION('center_axis',(1.,0.,0.));
#22776=DIRECTION('ref_axis',(0.,0.,1.));
#22777=DIRECTION('',(0.,-1.,0.));
#22778=DIRECTION('',(0.,0.,1.));
#22779=DIRECTION('center_axis',(-1.,0.,1.60844785188215E-15));
#22780=DIRECTION('ref_axis',(-1.60844785188215E-15,0.,-1.));
#22781=DIRECTION('',(0.,-1.,0.));
#22782=DIRECTION('',(-1.60844785188215E-15,0.,-1.));
#22783=DIRECTION('',(0.,-1.,0.));
#22784=DIRECTION('center_axis',(-0.707106781186546,0.,-0.707106781186549));
#22785=DIRECTION('ref_axis',(0.707106781186549,0.,-0.707106781186546));
#22786=DIRECTION('',(0.,-1.,0.));
#22787=DIRECTION('',(0.707106781186549,0.,-0.707106781186546));
#22788=DIRECTION('center_axis',(-1.55356845212375E-15,0.,-1.));
#22789=DIRECTION('ref_axis',(1.,0.,-1.55356845212375E-15));
#22790=DIRECTION('',(0.,-1.,0.));
#22791=DIRECTION('',(1.,0.,-1.55356845212375E-15));
#22792=DIRECTION('center_axis',(0.709478283082608,0.,-0.704727298913668));
#22793=DIRECTION('ref_axis',(0.704727298913668,0.,0.709478283082608));
#22794=DIRECTION('',(0.,-1.,0.));
#22795=DIRECTION('',(0.704727298913668,0.,0.709478283082608));
#22796=DIRECTION('center_axis',(0.,-1.,0.));
#22797=DIRECTION('ref_axis',(0.709478283082593,0.,-0.704727298913683));
#22798=DIRECTION('',(0.,-1.,0.));
#22799=DIRECTION('center_axis',(0.,-1.,0.));
#22800=DIRECTION('ref_axis',(0.709478283082593,0.,-0.704727298913683));
#22801=DIRECTION('center_axis',(0.707106781186548,0.,0.707106781186548));
#22802=DIRECTION('ref_axis',(-0.707106781186548,0.,0.707106781186548));
#22803=DIRECTION('',(0.,-1.,0.));
#22804=DIRECTION('',(-0.707106781186548,0.,0.707106781186548));
#22805=DIRECTION('center_axis',(0.,0.,1.));
#22806=DIRECTION('ref_axis',(-1.,0.,0.));
#22807=DIRECTION('',(0.,-1.,0.));
#22808=DIRECTION('',(-1.,0.,0.));
#22809=DIRECTION('center_axis',(-0.707106781186544,0.,0.707106781186551));
#22810=DIRECTION('ref_axis',(-0.707106781186551,0.,-0.707106781186544));
#22811=DIRECTION('',(-0.707106781186551,0.,-0.707106781186544));
#22812=DIRECTION('center_axis',(1.,0.,0.));
#22813=DIRECTION('ref_axis',(0.,0.,1.));
#22814=DIRECTION('',(0.,1.,0.));
#22815=DIRECTION('',(0.,0.,1.));
#22816=DIRECTION('center_axis',(-6.14369354430926E-16,0.,-1.));
#22817=DIRECTION('ref_axis',(1.,0.,-6.14369354430926E-16));
#22818=DIRECTION('',(1.,0.,-6.14369354430926E-16));
#22819=DIRECTION('',(0.,-1.,0.));
#22820=DIRECTION('center_axis',(0.710729249896223,0.,-0.703465658964212));
#22821=DIRECTION('ref_axis',(0.703465658964212,0.,0.710729249896223));
#22822=DIRECTION('',(0.703465658964212,0.,0.710729249896223));
#22823=DIRECTION('',(0.,-1.,0.));
#22824=DIRECTION('center_axis',(0.,-1.,0.));
#22825=DIRECTION('ref_axis',(-0.710729249896308,0.,0.703465658964126));
#22826=DIRECTION('center_axis',(0.,1.,0.));
#22827=DIRECTION('ref_axis',(-0.710729249896308,0.,0.703465658964126));
#22828=DIRECTION('',(0.,-1.,0.));
#22829=DIRECTION('center_axis',(0.,-1.,0.));
#22830=DIRECTION('ref_axis',(0.295138112194494,0.,-0.955454601082788));
#22831=DIRECTION('center_axis',(0.,-1.,0.));
#22832=DIRECTION('ref_axis',(0.295138112194494,0.,-0.955454601082788));
#22833=DIRECTION('',(0.,-1.,0.));
#22834=DIRECTION('center_axis',(0.,-1.,0.));
#22835=DIRECTION('ref_axis',(-0.295138112194515,0.,0.955454601082782));
#22836=DIRECTION('center_axis',(0.,1.,0.));
#22837=DIRECTION('ref_axis',(-0.295138112194515,0.,0.955454601082782));
#22838=DIRECTION('',(0.,-1.,0.));
#22839=DIRECTION('center_axis',(1.,0.,-1.93287220490857E-14));
#22840=DIRECTION('ref_axis',(1.93287220490857E-14,0.,1.));
#22841=DIRECTION('',(1.93287220490857E-14,0.,1.));
#22842=DIRECTION('',(0.,-1.,0.));
#22843=DIRECTION('center_axis',(0.,-1.,0.));
#22844=DIRECTION('ref_axis',(-1.,0.,1.48029736616691E-14));
#22845=DIRECTION('center_axis',(0.,1.,0.));
#22846=DIRECTION('ref_axis',(-1.,0.,1.48029736616691E-14));
#22847=DIRECTION('',(0.,-1.,0.));
#22848=DIRECTION('center_axis',(0.,-1.,0.));
#22849=DIRECTION('ref_axis',(0.951733868867033,0.,0.306924490471823));
#22850=DIRECTION('center_axis',(0.,-1.,0.));
#22851=DIRECTION('ref_axis',(0.951733868867033,0.,0.306924490471823));
#22852=DIRECTION('',(0.,-1.,0.));
#22853=DIRECTION('center_axis',(0.,-1.,0.));
#22854=DIRECTION('ref_axis',(-0.951733868867053,0.,-0.306924490471762));
#22855=DIRECTION('center_axis',(0.,1.,0.));
#22856=DIRECTION('ref_axis',(-0.951733868867053,0.,-0.306924490471762));
#22857=DIRECTION('',(0.,-1.,0.));
#22858=DIRECTION('center_axis',(0.711979844231348,0.,0.702199901316075));
#22859=DIRECTION('ref_axis',(-0.702199901316075,0.,0.711979844231348));
#22860=DIRECTION('',(-0.702199901316075,0.,0.711979844231348));
#22861=DIRECTION('',(0.,-1.,0.));
#22862=DIRECTION('center_axis',(0.,-1.,0.));
#22863=DIRECTION('ref_axis',(1.,0.,0.));
#22864=DIRECTION('center_axis',(0.,-1.,0.));
#22865=DIRECTION('ref_axis',(1.,0.,0.));
#22866=DIRECTION('center_axis',(0.,-1.,0.));
#22867=DIRECTION('ref_axis',(-1.,0.,0.));
#22868=DIRECTION('center_axis',(-0.710729249896204,0.,-0.703465658964231));
#22869=DIRECTION('ref_axis',(0.703465658964231,0.,-0.710729249896204));
#22870=DIRECTION('',(0.703465658964231,0.,-0.710729249896204));
#22871=DIRECTION('',(0.,-1.,0.));
#22872=DIRECTION('',(0.703465658964231,0.,-0.710729249896204));
#22873=DIRECTION('',(0.,-1.,0.));
#22874=DIRECTION('center_axis',(0.,-1.,0.));
#22875=DIRECTION('ref_axis',(0.963381374692962,0.,0.26813490428271));
#22876=DIRECTION('center_axis',(0.,1.,0.));
#22877=DIRECTION('ref_axis',(0.963381374692962,0.,0.26813490428271));
#22878=DIRECTION('center_axis',(0.,1.,0.));
#22879=DIRECTION('ref_axis',(0.963381374692962,0.,0.26813490428271));
#22880=DIRECTION('',(0.,-1.,0.));
#22881=DIRECTION('center_axis',(0.,-1.,0.));
#22882=DIRECTION('ref_axis',(-0.963381374692976,0.,-0.268134904282661));
#22883=DIRECTION('center_axis',(0.,-1.,0.));
#22884=DIRECTION('ref_axis',(-0.963381374692976,0.,-0.268134904282661));
#22885=DIRECTION('center_axis',(0.,-1.,0.));
#22886=DIRECTION('ref_axis',(-0.963381374692976,0.,-0.268134904282661));
#22887=DIRECTION('',(0.,-1.,0.));
#22888=DIRECTION('center_axis',(0.,-1.,0.));
#22889=DIRECTION('ref_axis',(1.,0.,0.));
#22890=DIRECTION('center_axis',(0.,1.,0.));
#22891=DIRECTION('ref_axis',(1.,0.,0.));
#22892=DIRECTION('center_axis',(0.,1.,0.));
#22893=DIRECTION('ref_axis',(1.,0.,0.));
#22894=DIRECTION('',(0.,-1.,0.));
#22895=DIRECTION('center_axis',(-1.,0.,0.));
#22896=DIRECTION('ref_axis',(0.,0.,-1.));
#22897=DIRECTION('',(0.,0.,-1.));
#22898=DIRECTION('',(0.,0.,-1.));
#22899=DIRECTION('',(0.,-1.,0.));
#22900=DIRECTION('center_axis',(0.,-1.,0.));
#22901=DIRECTION('ref_axis',(0.245760053518526,0.,-0.969330694909932));
#22902=DIRECTION('center_axis',(0.,1.,0.));
#22903=DIRECTION('ref_axis',(0.245760053518526,0.,-0.969330694909932));
#22904=DIRECTION('center_axis',(0.,1.,0.));
#22905=DIRECTION('ref_axis',(0.245760053518526,0.,-0.969330694909932));
#22906=DIRECTION('',(0.,-1.,0.));
#22907=DIRECTION('center_axis',(0.,-1.,0.));
#22908=DIRECTION('ref_axis',(-0.245760053518557,0.,0.969330694909924));
#22909=DIRECTION('center_axis',(0.,-1.,0.));
#22910=DIRECTION('ref_axis',(-0.245760053518557,0.,0.969330694909924));
#22911=DIRECTION('center_axis',(0.,-1.,0.));
#22912=DIRECTION('ref_axis',(-0.245760053518557,0.,0.969330694909924));
#22913=DIRECTION('',(0.,-1.,0.));
#22914=DIRECTION('center_axis',(0.,-1.,0.));
#22915=DIRECTION('ref_axis',(-1.,0.,0.));
#22916=DIRECTION('',(0.707106781186554,0.,0.707106781186541));
#22917=DIRECTION('',(0.,0.,1.));
#22918=DIRECTION('',(-0.707106781186548,0.,0.707106781186548));
#22919=DIRECTION('',(-1.,0.,0.));
#22920=DIRECTION('center_axis',(0.,1.,0.));
#22921=DIRECTION('ref_axis',(1.63979029060989E-14,0.,-1.));
#22922=DIRECTION('',(-1.,0.,0.));
#22923=DIRECTION('center_axis',(0.,-1.,0.));
#22924=DIRECTION('ref_axis',(-1.37675000001205E-14,0.,-1.));
#22925=DIRECTION('',(1.,0.,2.63040290597841E-15));
#22926=DIRECTION('',(0.707106781186546,0.,0.707106781186549));
#22927=DIRECTION('',(-2.63040290597841E-15,0.,1.));
#22928=DIRECTION('',(-0.707106781186556,0.,0.707106781186539));
#22929=DIRECTION('',(-1.60844785188215E-15,0.,-1.));
#22930=DIRECTION('',(0.707106781186549,0.,-0.707106781186546));
#22931=DIRECTION('',(1.,0.,-1.55356845212375E-15));
#22932=DIRECTION('',(0.704727298913668,0.,0.709478283082608));
#22933=DIRECTION('center_axis',(0.,-1.,0.));
#22934=DIRECTION('ref_axis',(0.709478283082593,0.,-0.704727298913683));
#22935=DIRECTION('',(0.,0.,1.));
#22936=DIRECTION('center_axis',(0.,-1.,0.));
#22937=DIRECTION('ref_axis',(1.,0.,0.));
#22938=DIRECTION('',(-0.702199901316075,0.,0.711979844231348));
#22939=DIRECTION('center_axis',(0.,1.,0.));
#22940=DIRECTION('ref_axis',(-0.951733868867053,0.,-0.306924490471762));
#22941=DIRECTION('center_axis',(0.,-1.,0.));
#22942=DIRECTION('ref_axis',(0.951733868867033,0.,0.306924490471823));
#22943=DIRECTION('center_axis',(0.,1.,0.));
#22944=DIRECTION('ref_axis',(-1.,0.,1.48029736616691E-14));
#22945=DIRECTION('',(1.93287220490857E-14,0.,1.));
#22946=DIRECTION('center_axis',(0.,1.,0.));
#22947=DIRECTION('ref_axis',(-0.295138112194515,0.,0.955454601082782));
#22948=DIRECTION('center_axis',(0.,-1.,0.));
#22949=DIRECTION('ref_axis',(0.295138112194494,0.,-0.955454601082788));
#22950=DIRECTION('center_axis',(0.,1.,0.));
#22951=DIRECTION('ref_axis',(-0.710729249896308,0.,0.703465658964126));
#22952=DIRECTION('',(0.703465658964212,0.,0.710729249896223));
#22953=DIRECTION('',(1.,0.,-6.14369354430926E-16));
#22954=DIRECTION('center_axis',(0.,1.,0.));
#22955=DIRECTION('ref_axis',(0.711979844231347,0.,-0.702199901316076));
#22956=DIRECTION('',(-0.702199901316085,0.,-0.711979844231338));
#22957=DIRECTION('center_axis',(0.,-1.,0.));
#22958=DIRECTION('ref_axis',(-0.711979844231317,0.,0.702199901316106));
#22959=DIRECTION('',(1.18143967662125E-14,0.,-1.));
#22960=DIRECTION('center_axis',(0.,-1.,0.));
#22961=DIRECTION('ref_axis',(-1.,0.,7.19001577852613E-14));
#22962=DIRECTION('',(0.70472729891367,0.,-0.709478283082607));
#22963=DIRECTION('',(1.,0.,0.));
#22964=DIRECTION('',(0.707106781186549,0.,0.707106781186546));
#22965=DIRECTION('',(0.,0.,1.));
#22966=DIRECTION('center_axis',(0.707106781186541,0.,-0.707106781186554));
#22967=DIRECTION('ref_axis',(0.707106781186554,0.,0.707106781186541));
#22968=DIRECTION('',(0.,-1.,0.));
#22969=DIRECTION('',(0.,-1.,0.));
#22970=DIRECTION('',(-0.707106781186554,0.,-0.707106781186541));
#22971=DIRECTION('center_axis',(1.,0.,0.));
#22972=DIRECTION('ref_axis',(0.,0.,1.));
#22973=DIRECTION('',(0.,-1.,0.));
#22974=DIRECTION('',(0.,0.,-1.));
#22975=DIRECTION('center_axis',(0.707106781186548,0.,0.707106781186548));
#22976=DIRECTION('ref_axis',(-0.707106781186548,0.,0.707106781186548));
#22977=DIRECTION('',(0.,-1.,0.));
#22978=DIRECTION('',(0.707106781186548,0.,-0.707106781186548));
#22979=DIRECTION('center_axis',(0.,0.,1.));
#22980=DIRECTION('ref_axis',(-1.,0.,0.));
#22981=DIRECTION('',(0.,-1.,0.));
#22982=DIRECTION('',(1.,0.,0.));
#22983=DIRECTION('center_axis',(0.,0.,-1.));
#22984=DIRECTION('ref_axis',(-1.,0.,0.));
#22985=DIRECTION('center_axis',(0.,0.,-1.));
#22986=DIRECTION('ref_axis',(-1.,0.,0.));
#22987=DIRECTION('center_axis',(0.,-1.,0.));
#22988=DIRECTION('ref_axis',(1.63979029060989E-14,0.,-1.));
#22989=DIRECTION('',(0.,-1.,0.));
#22990=DIRECTION('center_axis',(0.,-1.,0.));
#22991=DIRECTION('ref_axis',(1.63979029060989E-14,0.,-1.));
#22992=DIRECTION('center_axis',(0.,0.,1.));
#22993=DIRECTION('ref_axis',(-1.,0.,0.));
#22994=DIRECTION('',(-1.,0.,-2.63040290597841E-15));
#22995=DIRECTION('',(0.,-1.,0.));
#22996=DIRECTION('center_axis',(0.,-1.,0.));
#22997=DIRECTION('ref_axis',(-1.,0.,0.));
#22998=DIRECTION('',(0.,0.,1.));
#22999=DIRECTION('',(0.707106781186549,0.,0.707106781186546));
#23000=DIRECTION('',(1.,0.,0.));
#23001=DIRECTION('',(0.70472729891367,0.,-0.709478283082607));
#23002=DIRECTION('center_axis',(0.,-1.,0.));
#23003=DIRECTION('ref_axis',(-1.,0.,7.19001577852613E-14));
#23004=DIRECTION('',(1.18143967662125E-14,0.,-1.));
#23005=DIRECTION('center_axis',(0.,-1.,0.));
#23006=DIRECTION('ref_axis',(-0.711979844231317,0.,0.702199901316106));
#23007=DIRECTION('',(-0.702199901316085,0.,-0.711979844231338));
#23008=DIRECTION('center_axis',(0.,1.,0.));
#23009=DIRECTION('ref_axis',(0.711979844231347,0.,-0.702199901316076));
#23010=DIRECTION('',(1.,0.,-6.14369354430926E-16));
#23011=DIRECTION('',(0.703465658964212,0.,0.710729249896223));
#23012=DIRECTION('center_axis',(0.,1.,0.));
#23013=DIRECTION('ref_axis',(-0.710729249896308,0.,0.703465658964126));
#23014=DIRECTION('center_axis',(0.,-1.,0.));
#23015=DIRECTION('ref_axis',(0.295138112194494,0.,-0.955454601082788));
#23016=DIRECTION('center_axis',(0.,1.,0.));
#23017=DIRECTION('ref_axis',(-0.295138112194515,0.,0.955454601082782));
#23018=DIRECTION('',(1.93287220490857E-14,0.,1.));
#23019=DIRECTION('center_axis',(0.,1.,0.));
#23020=DIRECTION('ref_axis',(-1.,0.,1.48029736616691E-14));
#23021=DIRECTION('center_axis',(0.,-1.,0.));
#23022=DIRECTION('ref_axis',(0.951733868867033,0.,0.306924490471823));
#23023=DIRECTION('center_axis',(0.,1.,0.));
#23024=DIRECTION('ref_axis',(-0.951733868867053,0.,-0.306924490471762));
#23025=DIRECTION('',(-0.702199901316075,0.,0.711979844231348));
#23026=DIRECTION('center_axis',(0.,-1.,0.));
#23027=DIRECTION('ref_axis',(1.,0.,0.));
#23028=DIRECTION('',(0.,0.,1.));
#23029=DIRECTION('center_axis',(0.,-1.,0.));
#23030=DIRECTION('ref_axis',(0.709478283082593,0.,-0.704727298913683));
#23031=DIRECTION('',(0.704727298913668,0.,0.709478283082608));
#23032=DIRECTION('',(1.,0.,-1.55356845212375E-15));
#23033=DIRECTION('',(0.707106781186549,0.,-0.707106781186546));
#23034=DIRECTION('',(-1.60844785188215E-15,0.,-1.));
#23035=DIRECTION('',(0.707106781186556,0.,-0.707106781186539));
#23036=DIRECTION('',(2.63040290597841E-15,0.,-1.));
#23037=DIRECTION('',(-0.707106781186546,0.,-0.707106781186549));
#23038=DIRECTION('',(-1.,0.,-2.63040290597841E-15));
#23039=DIRECTION('center_axis',(0.,1.,0.));
#23040=DIRECTION('ref_axis',(-1.37675000001205E-14,0.,-1.));
#23041=DIRECTION('center_axis',(0.707106781186539,0.,0.707106781186556));
#23042=DIRECTION('ref_axis',(-0.707106781186556,0.,0.707106781186539));
#23043=DIRECTION('',(0.,-1.,0.));
#23044=DIRECTION('',(0.,1.,0.));
#23045=DIRECTION('center_axis',(1.,0.,2.63040290597841E-15));
#23046=DIRECTION('ref_axis',(-2.63040290597841E-15,0.,1.));
#23047=DIRECTION('',(0.,-1.,0.));
#23048=DIRECTION('center_axis',(0.707106781186549,0.,-0.707106781186546));
#23049=DIRECTION('ref_axis',(0.707106781186546,0.,0.707106781186549));
#23050=DIRECTION('',(0.,-1.,0.));
#23051=DIRECTION('center_axis',(2.63040290597841E-15,0.,-1.));
#23052=DIRECTION('ref_axis',(1.,0.,2.63040290597841E-15));
#23053=DIRECTION('',(0.,-1.,0.));
#23054=DIRECTION('center_axis',(2.63040290597841E-15,0.,-1.));
#23055=DIRECTION('ref_axis',(-1.,0.,0.));
#23056=DIRECTION('center_axis',(2.63040290597841E-15,0.,-1.));
#23057=DIRECTION('ref_axis',(-1.,0.,0.));
#23058=DIRECTION('center_axis',(0.,1.,0.));
#23059=DIRECTION('ref_axis',(-1.37675000001205E-14,0.,-1.));
#23060=DIRECTION('center_axis',(0.,0.,-1.));
#23061=DIRECTION('ref_axis',(-1.,0.,0.));
#23062=DIRECTION('',(0.,0.,-1.));
#23063=DIRECTION('center_axis',(0.,0.,1.));
#23064=DIRECTION('ref_axis',(-1.,0.,0.));
#23065=DIRECTION('center_axis',(0.,0.,-1.));
#23066=DIRECTION('ref_axis',(-1.,0.,0.));
#23067=DIRECTION('',(0.,0.,-1.));
#23068=DIRECTION('center_axis',(1.55356845212375E-15,0.,1.));
#23069=DIRECTION('ref_axis',(-1.,0.,0.));
#23070=DIRECTION('center_axis',(0.,0.,-1.));
#23071=DIRECTION('ref_axis',(-1.,0.,0.));
#23072=DIRECTION('',(0.,0.,-1.));
#23073=DIRECTION('center_axis',(0.,0.,1.));
#23074=DIRECTION('ref_axis',(-1.,0.,0.));
#23075=DIRECTION('center_axis',(0.,0.,-1.));
#23076=DIRECTION('ref_axis',(-1.,0.,0.));
#23077=DIRECTION('',(0.,0.,-1.));
#23078=DIRECTION('center_axis',(1.55356845212375E-15,0.,1.));
#23079=DIRECTION('ref_axis',(-1.,0.,0.));
#23080=DIRECTION('center_axis',(1.,0.,0.));
#23081=DIRECTION('ref_axis',(0.,0.,1.));
#23082=DIRECTION('',(0.,-1.,0.));
#23083=DIRECTION('center_axis',(0.707106781186546,0.,-0.707106781186549));
#23084=DIRECTION('ref_axis',(0.707106781186549,0.,0.707106781186546));
#23085=DIRECTION('',(0.,-1.,0.));
#23086=DIRECTION('center_axis',(0.,0.,-1.));
#23087=DIRECTION('ref_axis',(1.,0.,0.));
#23088=DIRECTION('',(0.,-1.,0.));
#23089=DIRECTION('center_axis',(-0.709478283082607,0.,-0.70472729891367));
#23090=DIRECTION('ref_axis',(0.70472729891367,0.,-0.709478283082607));
#23091=DIRECTION('',(0.,-1.,0.));
#23092=DIRECTION('center_axis',(0.,-1.,0.));
#23093=DIRECTION('ref_axis',(-1.,0.,7.19001577852613E-14));
#23094=DIRECTION('',(0.,-1.,0.));
#23095=DIRECTION('center_axis',(-1.,0.,-1.18143967662125E-14));
#23096=DIRECTION('ref_axis',(1.18143967662125E-14,0.,-1.));
#23097=DIRECTION('',(0.,-1.,0.));
#23098=DIRECTION('center_axis',(0.,-1.,0.));
#23099=DIRECTION('ref_axis',(-0.711979844231317,0.,0.702199901316106));
#23100=DIRECTION('',(0.,-1.,0.));
#23101=DIRECTION('center_axis',(-0.711979844231338,0.,0.702199901316085));
#23102=DIRECTION('ref_axis',(-0.702199901316085,0.,-0.711979844231338));
#23103=DIRECTION('',(0.,-1.,0.));
#23104=DIRECTION('center_axis',(0.,-1.,0.));
#23105=DIRECTION('ref_axis',(0.711979844231347,0.,-0.702199901316076));
#23106=DIRECTION('center_axis',(-1.,0.,1.60844785188215E-15));
#23107=DIRECTION('ref_axis',(-1.60844785188215E-15,0.,-1.));
#23108=DIRECTION('',(0.,-1.,0.));
#23109=DIRECTION('center_axis',(-0.707106781186546,0.,-0.707106781186549));
#23110=DIRECTION('ref_axis',(0.707106781186549,0.,-0.707106781186546));
#23111=DIRECTION('',(0.,-1.,0.));
#23112=DIRECTION('center_axis',(-1.55356845212375E-15,0.,-1.));
#23113=DIRECTION('ref_axis',(1.,0.,-1.55356845212375E-15));
#23114=DIRECTION('',(0.,-1.,0.));
#23115=DIRECTION('center_axis',(0.709478283082608,0.,-0.704727298913668));
#23116=DIRECTION('ref_axis',(0.704727298913668,0.,0.709478283082608));
#23117=DIRECTION('',(0.,-1.,0.));
#23118=DIRECTION('center_axis',(0.,-1.,0.));
#23119=DIRECTION('ref_axis',(0.709478283082593,0.,-0.704727298913683));
#23120=DIRECTION('',(0.,-1.,0.));
#23121=DIRECTION('center_axis',(1.,0.,0.));
#23122=DIRECTION('ref_axis',(0.,0.,1.));
#23123=DIRECTION('',(0.,1.,0.));
#23124=DIRECTION('center_axis',(0.,-1.,0.));
#23125=DIRECTION('ref_axis',(1.,0.,0.));
#23126=DIRECTION('',(0.,-1.,0.));
#23127=DIRECTION('center_axis',(0.711979844231348,0.,0.702199901316075));
#23128=DIRECTION('ref_axis',(-0.702199901316075,0.,0.711979844231348));
#23129=DIRECTION('',(0.,-1.,0.));
#23130=DIRECTION('center_axis',(0.,-1.,0.));
#23131=DIRECTION('ref_axis',(-0.951733868867053,0.,-0.306924490471762));
#23132=DIRECTION('',(0.,-1.,0.));
#23133=DIRECTION('center_axis',(0.,-1.,0.));
#23134=DIRECTION('ref_axis',(0.951733868867033,0.,0.306924490471823));
#23135=DIRECTION('',(0.,-1.,0.));
#23136=DIRECTION('center_axis',(0.,-1.,0.));
#23137=DIRECTION('ref_axis',(-1.,0.,1.48029736616691E-14));
#23138=DIRECTION('',(0.,-1.,0.));
#23139=DIRECTION('center_axis',(1.,0.,-1.93287220490857E-14));
#23140=DIRECTION('ref_axis',(1.93287220490857E-14,0.,1.));
#23141=DIRECTION('',(0.,-1.,0.));
#23142=DIRECTION('center_axis',(0.,-1.,0.));
#23143=DIRECTION('ref_axis',(-0.295138112194515,0.,0.955454601082782));
#23144=DIRECTION('',(0.,-1.,0.));
#23145=DIRECTION('center_axis',(0.,-1.,0.));
#23146=DIRECTION('ref_axis',(0.295138112194494,0.,-0.955454601082788));
#23147=DIRECTION('',(0.,-1.,0.));
#23148=DIRECTION('center_axis',(0.,-1.,0.));
#23149=DIRECTION('ref_axis',(-0.710729249896308,0.,0.703465658964126));
#23150=DIRECTION('',(0.,-1.,0.));
#23151=DIRECTION('center_axis',(0.710729249896223,0.,-0.703465658964212));
#23152=DIRECTION('ref_axis',(0.703465658964212,0.,0.710729249896223));
#23153=DIRECTION('',(0.,-1.,0.));
#23154=DIRECTION('center_axis',(-6.14369354430926E-16,0.,-1.));
#23155=DIRECTION('ref_axis',(1.,0.,-6.14369354430926E-16));
#23156=DIRECTION('center_axis',(0.,-1.,0.));
#23157=DIRECTION('ref_axis',(0.711979844231347,0.,-0.702199901316076));
#23158=DIRECTION('center_axis',(0.,1.,0.));
#23159=DIRECTION('ref_axis',(0.711979844231347,0.,-0.702199901316076));
#23160=DIRECTION('',(0.,-1.,0.));
#23161=DIRECTION('center_axis',(0.,-1.,0.));
#23162=DIRECTION('ref_axis',(0.711979844231347,0.,-0.702199901316076));
#23163=DIRECTION('',(0.,-1.,0.));
#23164=DIRECTION('center_axis',(-0.711979844231338,0.,0.702199901316085));
#23165=DIRECTION('ref_axis',(-0.702199901316085,0.,-0.711979844231338));
#23166=DIRECTION('',(-0.702199901316085,0.,-0.711979844231338));
#23167=DIRECTION('',(0.702199901316085,0.,0.711979844231338));
#23168=DIRECTION('',(0.,-1.,0.));
#23169=DIRECTION('center_axis',(0.,-1.,0.));
#23170=DIRECTION('ref_axis',(-0.711979844231317,0.,0.702199901316106));
#23171=DIRECTION('center_axis',(0.,-1.,0.));
#23172=DIRECTION('ref_axis',(-0.711979844231317,0.,0.702199901316106));
#23173=DIRECTION('center_axis',(0.,1.,0.));
#23174=DIRECTION('ref_axis',(-0.711979844231317,0.,0.702199901316106));
#23175=DIRECTION('',(0.,-1.,0.));
#23176=DIRECTION('center_axis',(-1.,0.,-1.18143967662125E-14));
#23177=DIRECTION('ref_axis',(1.18143967662125E-14,0.,-1.));
#23178=DIRECTION('',(1.18143967662125E-14,0.,-1.));
#23179=DIRECTION('',(-1.18143967662125E-14,0.,1.));
#23180=DIRECTION('',(0.,-1.,0.));
#23181=DIRECTION('center_axis',(0.,-1.,0.));
#23182=DIRECTION('ref_axis',(-1.,0.,7.19001577852613E-14));
#23183=DIRECTION('center_axis',(0.,-1.,0.));
#23184=DIRECTION('ref_axis',(-1.,0.,7.19001577852613E-14));
#23185=DIRECTION('center_axis',(0.,1.,0.));
#23186=DIRECTION('ref_axis',(-1.,0.,7.19001577852613E-14));
#23187=DIRECTION('',(0.,-1.,0.));
#23188=DIRECTION('center_axis',(-0.709478283082607,0.,-0.70472729891367));
#23189=DIRECTION('ref_axis',(0.70472729891367,0.,-0.709478283082607));
#23190=DIRECTION('',(0.70472729891367,0.,-0.709478283082607));
#23191=DIRECTION('',(-0.70472729891367,0.,0.709478283082607));
#23192=DIRECTION('',(0.,-1.,0.));
#23193=DIRECTION('center_axis',(0.,0.,-1.));
#23194=DIRECTION('ref_axis',(1.,0.,0.));
#23195=DIRECTION('',(1.,0.,0.));
#23196=DIRECTION('',(-1.,0.,0.));
#23197=DIRECTION('',(0.,-1.,0.));
#23198=DIRECTION('center_axis',(0.707106781186546,0.,-0.707106781186549));
#23199=DIRECTION('ref_axis',(0.707106781186549,0.,0.707106781186546));
#23200=DIRECTION('',(0.707106781186549,0.,0.707106781186546));
#23201=DIRECTION('',(-0.707106781186549,0.,-0.707106781186546));
#23202=DIRECTION('',(0.,-1.,0.));
#23203=DIRECTION('center_axis',(0.707106781186548,0.,0.707106781186548));
#23204=DIRECTION('ref_axis',(-0.707106781186548,0.,0.707106781186548));
#23205=DIRECTION('',(0.707106781186548,0.,-0.707106781186548));
#23206=DIRECTION('',(0.,-1.,0.));
#23207=DIRECTION('',(0.707106781186548,0.,-0.707106781186548));
#23208=DIRECTION('',(0.,-1.,0.));
#23209=DIRECTION('center_axis',(0.,0.,1.));
#23210=DIRECTION('ref_axis',(-1.,0.,0.));
#23211=DIRECTION('',(1.,0.,0.));
#23212=DIRECTION('',(1.,0.,0.));
#23213=DIRECTION('',(0.,-1.,0.));
#23214=DIRECTION('center_axis',(-0.707106781186544,0.,0.707106781186551));
#23215=DIRECTION('ref_axis',(-0.707106781186551,0.,-0.707106781186544));
#23216=DIRECTION('',(0.707106781186551,0.,0.707106781186544));
#23217=DIRECTION('',(0.707106781186551,0.,0.707106781186544));
#23218=DIRECTION('',(0.,-1.,0.));
#23219=DIRECTION('center_axis',(-1.,0.,1.60844785188215E-15));
#23220=DIRECTION('ref_axis',(-1.60844785188215E-15,0.,-1.));
#23221=DIRECTION('',(-1.60844785188215E-15,0.,-1.));
#23222=DIRECTION('',(1.60844785188215E-15,0.,1.));
#23223=DIRECTION('',(0.,-1.,0.));
#23224=DIRECTION('center_axis',(-0.707106781186546,0.,-0.707106781186549));
#23225=DIRECTION('ref_axis',(0.707106781186549,0.,-0.707106781186546));
#23226=DIRECTION('',(0.707106781186549,0.,-0.707106781186546));
#23227=DIRECTION('',(-0.707106781186549,0.,0.707106781186546));
#23228=DIRECTION('',(0.,-1.,0.));
#23229=DIRECTION('center_axis',(-1.55356845212375E-15,0.,-1.));
#23230=DIRECTION('ref_axis',(1.,0.,-1.55356845212375E-15));
#23231=DIRECTION('',(1.,0.,-1.55356845212375E-15));
#23232=DIRECTION('',(-1.,0.,1.55356845212375E-15));
#23233=DIRECTION('',(0.,-1.,0.));
#23234=DIRECTION('center_axis',(0.709478283082608,0.,-0.704727298913668));
#23235=DIRECTION('ref_axis',(0.704727298913668,0.,0.709478283082608));
#23236=DIRECTION('',(0.704727298913668,0.,0.709478283082608));
#23237=DIRECTION('',(-0.704727298913668,0.,-0.709478283082608));
#23238=DIRECTION('',(0.,-1.,0.));
#23239=DIRECTION('center_axis',(0.,-1.,0.));
#23240=DIRECTION('ref_axis',(0.709478283082593,0.,-0.704727298913683));
#23241=DIRECTION('center_axis',(0.,-1.,0.));
#23242=DIRECTION('ref_axis',(0.709478283082593,0.,-0.704727298913683));
#23243=DIRECTION('center_axis',(0.,1.,0.));
#23244=DIRECTION('ref_axis',(0.709478283082593,0.,-0.704727298913683));
#23245=DIRECTION('',(0.,-1.,0.));
#23246=DIRECTION('center_axis',(0.,-1.,0.));
#23247=DIRECTION('ref_axis',(-1.,0.,0.));
#23248=DIRECTION('center_axis',(0.,1.,0.));
#23249=DIRECTION('ref_axis',(1.,0.,0.));
#23250=DIRECTION('',(0.,0.,-1.));
#23251=DIRECTION('',(0.,0.,-1.));
#23252=DIRECTION('center_axis',(0.,1.,0.));
#23253=DIRECTION('ref_axis',(-0.245760053518557,0.,0.969330694909924));
#23254=DIRECTION('center_axis',(0.,-1.,0.));
#23255=DIRECTION('ref_axis',(0.245760053518526,0.,-0.969330694909932));
#23256=DIRECTION('',(0.,0.,1.));
#23257=DIRECTION('center_axis',(0.,-1.,0.));
#23258=DIRECTION('ref_axis',(1.,0.,0.));
#23259=DIRECTION('center_axis',(0.,1.,0.));
#23260=DIRECTION('ref_axis',(-0.963381374692976,0.,-0.268134904282661));
#23261=DIRECTION('center_axis',(0.,-1.,0.));
#23262=DIRECTION('ref_axis',(0.963381374692962,0.,0.26813490428271));
#23263=DIRECTION('',(-0.703465658964231,0.,0.710729249896204));
#23264=DIRECTION('',(-1.,0.,6.14369354430926E-16));
#23265=DIRECTION('',(-0.703465658964212,0.,-0.710729249896223));
#23266=DIRECTION('center_axis',(0.,-1.,0.));
#23267=DIRECTION('ref_axis',(-0.710729249896308,0.,0.703465658964126));
#23268=DIRECTION('center_axis',(0.,1.,0.));
#23269=DIRECTION('ref_axis',(0.295138112194494,0.,-0.955454601082788));
#23270=DIRECTION('center_axis',(0.,-1.,0.));
#23271=DIRECTION('ref_axis',(-0.295138112194515,0.,0.955454601082782));
#23272=DIRECTION('',(-1.93287220490857E-14,0.,-1.));
#23273=DIRECTION('center_axis',(0.,-1.,0.));
#23274=DIRECTION('ref_axis',(-1.,0.,1.48029736616691E-14));
#23275=DIRECTION('center_axis',(0.,1.,0.));
#23276=DIRECTION('ref_axis',(0.951733868867033,0.,0.306924490471823));
#23277=DIRECTION('center_axis',(0.,-1.,0.));
#23278=DIRECTION('ref_axis',(-0.951733868867053,0.,-0.306924490471762));
#23279=DIRECTION('',(0.702199901316075,0.,-0.711979844231348));
#23280=DIRECTION('center_axis',(1.,0.,0.));
#23281=DIRECTION('ref_axis',(0.,0.,1.));
#23282=DIRECTION('',(0.,0.,1.));
#23283=DIRECTION('center_axis',(1.,0.,0.));
#23284=DIRECTION('ref_axis',(0.,0.,1.));
#23285=DIRECTION('',(0.,0.,1.));
#23286=DIRECTION('',(0.,1.,0.));
#23287=DIRECTION('center_axis',(0.,-1.,0.));
#23288=DIRECTION('ref_axis',(1.,0.,0.));
#23289=DIRECTION('center_axis',(0.,-1.,0.));
#23290=DIRECTION('ref_axis',(1.,0.,0.));
#23291=DIRECTION('',(0.,-1.,0.));
#23292=DIRECTION('center_axis',(0.711979844231348,0.,0.702199901316075));
#23293=DIRECTION('ref_axis',(-0.702199901316075,0.,0.711979844231348));
#23294=DIRECTION('',(-0.702199901316075,0.,0.711979844231348));
#23295=DIRECTION('',(0.,-1.,0.));
#23296=DIRECTION('center_axis',(0.,-1.,0.));
#23297=DIRECTION('ref_axis',(-0.951733868867053,0.,-0.306924490471762));
#23298=DIRECTION('center_axis',(0.,1.,0.));
#23299=DIRECTION('ref_axis',(-0.951733868867053,0.,-0.306924490471762));
#23300=DIRECTION('',(0.,-1.,0.));
#23301=DIRECTION('center_axis',(0.,-1.,0.));
#23302=DIRECTION('ref_axis',(0.951733868867033,0.,0.306924490471823));
#23303=DIRECTION('center_axis',(0.,-1.,0.));
#23304=DIRECTION('ref_axis',(0.951733868867033,0.,0.306924490471823));
#23305=DIRECTION('',(0.,-1.,0.));
#23306=DIRECTION('center_axis',(0.,-1.,0.));
#23307=DIRECTION('ref_axis',(-1.,0.,1.48029736616691E-14));
#23308=DIRECTION('center_axis',(0.,1.,0.));
#23309=DIRECTION('ref_axis',(-1.,0.,1.48029736616691E-14));
#23310=DIRECTION('',(0.,-1.,0.));
#23311=DIRECTION('center_axis',(1.,0.,-1.93287220490857E-14));
#23312=DIRECTION('ref_axis',(1.93287220490857E-14,0.,1.));
#23313=DIRECTION('',(1.93287220490857E-14,0.,1.));
#23314=DIRECTION('',(0.,-1.,0.));
#23315=DIRECTION('center_axis',(0.,-1.,0.));
#23316=DIRECTION('ref_axis',(-0.295138112194515,0.,0.955454601082782));
#23317=DIRECTION('center_axis',(0.,1.,0.));
#23318=DIRECTION('ref_axis',(-0.295138112194515,0.,0.955454601082782));
#23319=DIRECTION('',(0.,-1.,0.));
#23320=DIRECTION('center_axis',(0.,-1.,0.));
#23321=DIRECTION('ref_axis',(0.295138112194494,0.,-0.955454601082788));
#23322=DIRECTION('center_axis',(0.,-1.,0.));
#23323=DIRECTION('ref_axis',(0.295138112194494,0.,-0.955454601082788));
#23324=DIRECTION('',(0.,-1.,0.));
#23325=DIRECTION('center_axis',(0.,-1.,0.));
#23326=DIRECTION('ref_axis',(-0.710729249896308,0.,0.703465658964126));
#23327=DIRECTION('center_axis',(0.,1.,0.));
#23328=DIRECTION('ref_axis',(-0.710729249896308,0.,0.703465658964126));
#23329=DIRECTION('',(0.,-1.,0.));
#23330=DIRECTION('center_axis',(0.710729249896223,0.,-0.703465658964212));
#23331=DIRECTION('ref_axis',(0.703465658964212,0.,0.710729249896223));
#23332=DIRECTION('',(0.703465658964212,0.,0.710729249896223));
#23333=DIRECTION('',(0.,-1.,0.));
#23334=DIRECTION('center_axis',(-6.14369354430926E-16,0.,-1.));
#23335=DIRECTION('ref_axis',(1.,0.,-6.14369354430926E-16));
#23336=DIRECTION('',(1.,0.,-6.14369354430926E-16));
#23337=DIRECTION('',(0.,-1.,0.));
#23338=DIRECTION('center_axis',(-0.710729249896204,0.,-0.703465658964231));
#23339=DIRECTION('ref_axis',(0.703465658964231,0.,-0.710729249896204));
#23340=DIRECTION('',(0.703465658964231,0.,-0.710729249896204));
#23341=DIRECTION('',(0.,-1.,0.));
#23342=DIRECTION('center_axis',(0.,-1.,0.));
#23343=DIRECTION('ref_axis',(0.963381374692962,0.,0.26813490428271));
#23344=DIRECTION('center_axis',(0.,1.,0.));
#23345=DIRECTION('ref_axis',(0.963381374692962,0.,0.26813490428271));
#23346=DIRECTION('',(0.,-1.,0.));
#23347=DIRECTION('center_axis',(0.,-1.,0.));
#23348=DIRECTION('ref_axis',(-0.963381374692976,0.,-0.268134904282661));
#23349=DIRECTION('center_axis',(0.,-1.,0.));
#23350=DIRECTION('ref_axis',(-0.963381374692976,0.,-0.268134904282661));
#23351=DIRECTION('',(0.,-1.,0.));
#23352=DIRECTION('center_axis',(0.,-1.,0.));
#23353=DIRECTION('ref_axis',(1.,0.,0.));
#23354=DIRECTION('center_axis',(0.,1.,0.));
#23355=DIRECTION('ref_axis',(1.,0.,0.));
#23356=DIRECTION('',(0.,-1.,0.));
#23357=DIRECTION('center_axis',(-1.,0.,0.));
#23358=DIRECTION('ref_axis',(0.,0.,-1.));
#23359=DIRECTION('',(0.,0.,-1.));
#23360=DIRECTION('',(0.,-1.,0.));
#23361=DIRECTION('center_axis',(0.,-1.,0.));
#23362=DIRECTION('ref_axis',(0.245760053518526,0.,-0.969330694909932));
#23363=DIRECTION('center_axis',(0.,1.,0.));
#23364=DIRECTION('ref_axis',(0.245760053518526,0.,-0.969330694909932));
#23365=DIRECTION('',(0.,-1.,0.));
#23366=DIRECTION('center_axis',(0.,-1.,0.));
#23367=DIRECTION('ref_axis',(-0.245760053518557,0.,0.969330694909924));
#23368=DIRECTION('center_axis',(0.,-1.,0.));
#23369=DIRECTION('ref_axis',(-0.245760053518557,0.,0.969330694909924));
#23370=DIRECTION('center_axis',(0.,-1.,0.));
#23371=DIRECTION('ref_axis',(1.,0.,0.));
#27875=CARTESIAN_POINT('',(0.,0.,0.));
#27876=CARTESIAN_POINT('Origin',(103.778785519041,230.,0.));
#27877=CARTESIAN_POINT('',(113.356459668193,230.,58.0910625167936));
#27878=CARTESIAN_POINT('',(113.356459668193,230.,36.0032237681315));
#27879=CARTESIAN_POINT('',(113.356459668193,230.,29.0455312583968));
#27880=CARTESIAN_POINT('',(114.356459668193,230.,59.0910625167936));
#27881=CARTESIAN_POINT('',(120.773904182304,230.,65.5085070309049));
#27882=CARTESIAN_POINT('',(155.375609963127,230.,59.0910625167936));
#27883=CARTESIAN_POINT('',(150.62266449878,230.,59.0910625167936));
#27884=CARTESIAN_POINT('',(156.375609963127,230.,58.0910625167936));
#27885=CARTESIAN_POINT('',(154.960007558403,230.,59.5066649215182));
#27886=CARTESIAN_POINT('',(156.375609963127,230.,36.0032237681314));
#27887=CARTESIAN_POINT('',(156.375609963127,230.,18.0016118840657));
#27888=CARTESIAN_POINT('',(154.875609963127,230.,34.5032237681314));
#27889=CARTESIAN_POINT('',(133.475597910073,230.,13.1032117150771));
#27890=CARTESIAN_POINT('',(144.417668112103,230.,34.5032237681314));
#27891=CARTESIAN_POINT('',(124.098226815572,230.,34.5032237681314));
#27892=CARTESIAN_POINT('',(141.763569006683,230.,37.1752157277839));
#27893=CARTESIAN_POINT('',(141.62477097808,230.,37.3149494761148));
#27894=CARTESIAN_POINT('',(141.458521203919,230.,37.9151793916432));
#27895=CARTESIAN_POINT('Origin',(142.508521203919,230.,37.9151793916432));
#27896=CARTESIAN_POINT('',(141.458521203919,230.,39.4187321117283));
#27897=CARTESIAN_POINT('',(141.45852120392,230.,19.7093660558644));
#27898=CARTESIAN_POINT('',(141.760942367476,230.,40.1560420081102));
#27899=CARTESIAN_POINT('Origin',(142.508521203919,230.,39.4187321117283));
#27900=CARTESIAN_POINT('',(142.398712869122,230.,40.8026951072716));
#27901=CARTESIAN_POINT('',(122.677567086127,230.,20.8068815557118));
#27902=CARTESIAN_POINT('',(142.734368503612,230.,41.3560806824536));
#27903=CARTESIAN_POINT('Origin',(141.401941087198,230.,41.7857749691141));
#27904=CARTESIAN_POINT('',(144.403306787367,230.,42.9220241352404));
#27905=CARTESIAN_POINT('Origin',(144.984289187872,230.,40.6305041508117));
#27906=CARTESIAN_POINT('',(144.855850755256,230.,43.5036225521863));
#27907=CARTESIAN_POINT('Origin',(144.255850755256,230.,43.5036225521863));
#27908=CARTESIAN_POINT('',(144.855850755256,230.,44.4226470147914));
#27909=CARTESIAN_POINT('',(144.855850755256,230.,22.2113235073957));
#27910=CARTESIAN_POINT('',(144.344825886597,230.,45.1153516005764));
#27911=CARTESIAN_POINT('Origin',(144.130850755256,230.,44.4226470147914));
#27912=CARTESIAN_POINT('',(142.695977084858,230.,46.8112703207193));
#27913=CARTESIAN_POINT('Origin',(145.073060872192,230.,47.4728765656934));
#27914=CARTESIAN_POINT('',(142.5822836287,230.,47.007169160326));
#27915=CARTESIAN_POINT('Origin',(142.262455466246,230.,46.690609613792));
#27916=CARTESIAN_POINT('',(142.094409841973,230.,47.5000804575095));
#27917=CARTESIAN_POINT('',(144.48829315277,230.,45.0814792533986));
#27918=CARTESIAN_POINT('',(127.637659789347,230.,47.5000804575095));
#27919=CARTESIAN_POINT('',(115.708222654194,230.,47.5000804575095));
#27920=CARTESIAN_POINT('',(127.149786002621,230.,47.007169160326));
#27921=CARTESIAN_POINT('',(109.61588112148,230.,29.2922190342974));
#27922=CARTESIAN_POINT('',(127.036092546462,230.,46.8112703207193));
#27923=CARTESIAN_POINT('Origin',(127.469614165074,230.,46.690609613792));
#27924=CARTESIAN_POINT('',(125.387243744723,230.,45.1153516005764));
#27925=CARTESIAN_POINT('Origin',(124.659008759128,230.,47.4728765656934));
#27926=CARTESIAN_POINT('',(124.876218876064,230.,44.4226470147914));
#27927=CARTESIAN_POINT('Origin',(125.601218876064,230.,44.4226470147914));
#27928=CARTESIAN_POINT('',(124.876218876064,230.,43.5036225521864));
#27929=CARTESIAN_POINT('',(124.876218876064,230.,21.751811276093));
#27930=CARTESIAN_POINT('',(125.328762843953,230.,42.9220241352404));
#27931=CARTESIAN_POINT('Origin',(125.476218876064,230.,43.5036225521863));
#27932=CARTESIAN_POINT('',(126.997701127708,230.,41.3560806824536));
#27933=CARTESIAN_POINT('Origin',(124.747780443448,230.,40.6305041508116));
#27934=CARTESIAN_POINT('',(127.333356762198,230.,40.8026951072716));
#27935=CARTESIAN_POINT('Origin',(128.330128544122,230.,41.785774969114));
#27936=CARTESIAN_POINT('',(127.971127263844,230.,40.1560420081102));
#27937=CARTESIAN_POINT('',(132.044740758987,230.,36.025692948968));
#27938=CARTESIAN_POINT('',(128.273548427401,230.,39.4187321117283));
#27939=CARTESIAN_POINT('Origin',(127.223548427401,230.,39.4187321117283));
#27940=CARTESIAN_POINT('',(128.273548427401,230.,37.9151793916432));
#27941=CARTESIAN_POINT('',(128.273548427401,230.,18.9575896958216));
#27942=CARTESIAN_POINT('',(127.968500624638,230.,37.1752157277839));
#27943=CARTESIAN_POINT('Origin',(127.223548427401,230.,37.9151793916432));
#27944=CARTESIAN_POINT('',(125.314401519217,230.,34.5032237681315));
#27945=CARTESIAN_POINT('',(111.34106001963,230.,20.435679696352));
#27946=CARTESIAN_POINT('',(114.856459668193,230.,34.5032237681315));
#27947=CARTESIAN_POINT('',(109.317622593617,230.,34.5032237681315));
#27948=CARTESIAN_POINT('',(119.962847072938,230.,29.3968363633866));
#27949=CARTESIAN_POINT('Origin',(142.094409841973,255.,47.5000804575095));
#27950=CARTESIAN_POINT('',(142.5822836287,216.,47.007169160326));
#27951=CARTESIAN_POINT('',(142.5822836287,255.,47.007169160326));
#27952=CARTESIAN_POINT('',(142.094409841973,216.,47.5000804575095));
#27953=CARTESIAN_POINT('',(142.5822836287,216.,47.007169160326));
#27954=CARTESIAN_POINT('',(142.094409841973,255.,47.5000804575095));
#27955=CARTESIAN_POINT('Origin',(142.262455466246,255.,46.690609613792));
#27956=CARTESIAN_POINT('',(142.695977084858,216.,46.8112703207193));
#27957=CARTESIAN_POINT('',(142.695977084858,255.,46.8112703207193));
#27958=CARTESIAN_POINT('Origin',(142.262455466246,216.,46.690609613792));
#27959=CARTESIAN_POINT('Origin',(145.073060872192,255.,47.4728765656934));
#27960=CARTESIAN_POINT('',(144.344825886597,216.,45.1153516005764));
#27961=CARTESIAN_POINT('',(144.344825886597,255.,45.1153516005764));
#27962=CARTESIAN_POINT('Origin',(145.073060872192,216.,47.4728765656934));
#27963=CARTESIAN_POINT('Origin',(144.130850755256,255.,44.4226470147914));
#27964=CARTESIAN_POINT('',(144.855850755256,216.,44.4226470147914));
#27965=CARTESIAN_POINT('',(144.855850755256,255.,44.4226470147914));
#27966=CARTESIAN_POINT('Origin',(144.130850755256,216.,44.4226470147914));
#27967=CARTESIAN_POINT('Origin',(144.855850755256,255.,44.4226470147914));
#27968=CARTESIAN_POINT('',(144.855850755256,216.,43.5036225521863));
#27969=CARTESIAN_POINT('',(144.855850755256,255.,43.5036225521863));
#27970=CARTESIAN_POINT('',(144.855850755256,216.,43.5036225521863));
#27971=CARTESIAN_POINT('Origin',(144.255850755256,255.,43.5036225521863));
#27972=CARTESIAN_POINT('',(144.403306787367,216.,42.9220241352404));
#27973=CARTESIAN_POINT('',(144.403306787367,255.,42.9220241352404));
#27974=CARTESIAN_POINT('Origin',(144.255850755256,216.,43.5036225521863));
#27975=CARTESIAN_POINT('Origin',(144.984289187872,255.,40.6305041508117));
#27976=CARTESIAN_POINT('',(142.734368503612,216.,41.3560806824536));
#27977=CARTESIAN_POINT('',(142.734368503612,255.,41.3560806824536));
#27978=CARTESIAN_POINT('Origin',(144.984289187872,216.,40.6305041508117));
#27979=CARTESIAN_POINT('Origin',(141.401941087198,255.,41.7857749691141));
#27980=CARTESIAN_POINT('',(142.398712869122,216.,40.8026951072716));
#27981=CARTESIAN_POINT('',(142.398712869122,255.,40.8026951072716));
#27982=CARTESIAN_POINT('Origin',(141.401941087198,216.,41.7857749691141));
#27983=CARTESIAN_POINT('Origin',(142.398712869122,255.,40.8026951072716));
#27984=CARTESIAN_POINT('',(141.760942367476,216.,40.1560420081102));
#27985=CARTESIAN_POINT('',(141.760942367476,255.,40.1560420081102));
#27986=CARTESIAN_POINT('',(141.760942367476,216.,40.1560420081102));
#27987=CARTESIAN_POINT('Origin',(142.508521203919,255.,39.4187321117283));
#27988=CARTESIAN_POINT('',(141.458521203919,216.,39.4187321117283));
#27989=CARTESIAN_POINT('',(141.458521203919,255.,39.4187321117283));
#27990=CARTESIAN_POINT('Origin',(142.508521203919,216.,39.4187321117283));
#27991=CARTESIAN_POINT('Origin',(141.458521203919,255.,39.4187321117283));
#27992=CARTESIAN_POINT('',(141.458521203919,216.,37.9151793916432));
#27993=CARTESIAN_POINT('',(141.458521203919,255.,37.9151793916432));
#27994=CARTESIAN_POINT('',(141.458521203919,216.,37.9151793916432));
#27995=CARTESIAN_POINT('Origin',(142.508521203919,255.,37.9151793916432));
#27996=CARTESIAN_POINT('',(141.763569006683,216.,37.1752157277839));
#27997=CARTESIAN_POINT('',(141.763569006683,255.,37.1752157277839));
#27998=CARTESIAN_POINT('Origin',(142.508521203919,216.,37.9151793916432));
#27999=CARTESIAN_POINT('Origin',(141.763569006683,255.,37.1752157277839));
#28000=CARTESIAN_POINT('',(144.417668112103,216.,34.5032237681314));
#28001=CARTESIAN_POINT('',(144.417668112103,255.,34.5032237681314));
#28002=CARTESIAN_POINT('',(144.544688744748,216.,34.375346814161));
#28003=CARTESIAN_POINT('Origin',(144.417668112103,255.,34.5032237681314));
#28004=CARTESIAN_POINT('',(154.875609963127,216.,34.5032237681314));
#28005=CARTESIAN_POINT('',(154.875609963127,255.,34.5032237681314));
#28006=CARTESIAN_POINT('',(134.86603481566,216.,34.5032237681314));
#28007=CARTESIAN_POINT('Origin',(154.875609963127,255.,34.5032237681314));
#28008=CARTESIAN_POINT('',(156.375609963127,216.,36.0032237681314));
#28009=CARTESIAN_POINT('',(156.375609963127,255.,36.0032237681314));
#28010=CARTESIAN_POINT('',(154.875609963127,216.,34.5032237681314));
#28011=CARTESIAN_POINT('Origin',(156.375609963127,255.,36.0032237681314));
#28012=CARTESIAN_POINT('',(156.375609963127,216.,58.0910625167936));
#28013=CARTESIAN_POINT('',(156.375609963127,255.,58.0910625167936));
#28014=CARTESIAN_POINT('',(156.375609963127,216.,36.0032237681314));
#28015=CARTESIAN_POINT('Origin',(113.356459668193,255.,58.0910625167937));
#28016=CARTESIAN_POINT('',(113.356459668193,216.,36.0032237681315));
#28017=CARTESIAN_POINT('',(113.356459668193,255.,36.0032237681315));
#28018=CARTESIAN_POINT('',(113.356459668193,216.,58.0910625167937));
#28019=CARTESIAN_POINT('',(113.356459668193,216.,36.0032237681315));
#28020=CARTESIAN_POINT('',(113.356459668193,255.,58.0910625167937));
#28021=CARTESIAN_POINT('Origin',(113.356459668193,255.,36.0032237681315));
#28022=CARTESIAN_POINT('',(114.856459668193,216.,34.5032237681315));
#28023=CARTESIAN_POINT('',(114.856459668193,255.,34.5032237681315));
#28024=CARTESIAN_POINT('',(114.856459668193,216.,34.5032237681315));
#28025=CARTESIAN_POINT('Origin',(114.856459668193,255.,34.5032237681315));
#28026=CARTESIAN_POINT('',(125.314401519217,216.,34.5032237681315));
#28027=CARTESIAN_POINT('',(125.314401519217,255.,34.5032237681315));
#28028=CARTESIAN_POINT('',(134.86603481566,216.,34.5032237681314));
#28029=CARTESIAN_POINT('Origin',(125.314401519217,255.,34.5032237681315));
#28030=CARTESIAN_POINT('',(127.968500624638,216.,37.1752157277839));
#28031=CARTESIAN_POINT('',(127.968500624638,255.,37.1752157277839));
#28032=CARTESIAN_POINT('',(127.968500624638,216.,37.1752157277839));
#28033=CARTESIAN_POINT('Origin',(127.223548427401,255.,37.9151793916432));
#28034=CARTESIAN_POINT('',(128.273548427401,216.,37.9151793916432));
#28035=CARTESIAN_POINT('',(128.273548427401,255.,37.9151793916432));
#28036=CARTESIAN_POINT('Origin',(127.223548427401,216.,37.9151793916432));
#28037=CARTESIAN_POINT('Origin',(156.375609963127,255.,58.0910625167936));
#28038=CARTESIAN_POINT('',(155.375609963127,216.,59.0910625167936));
#28039=CARTESIAN_POINT('',(155.375609963127,255.,59.0910625167936));
#28040=CARTESIAN_POINT('',(156.375609963127,216.,58.0910625167936));
#28041=CARTESIAN_POINT('Origin',(155.375609963127,255.,59.0910625167936));
#28042=CARTESIAN_POINT('',(114.356459668193,216.,59.0910625167936));
#28043=CARTESIAN_POINT('',(114.356459668193,255.,59.0910625167936));
#28044=CARTESIAN_POINT('',(155.375609963127,216.,59.0910625167936));
#28045=CARTESIAN_POINT('Origin',(114.356459668193,255.,59.0910625167936));
#28046=CARTESIAN_POINT('',(113.356459668193,216.,58.0910625167937));
#28047=CARTESIAN_POINT('Origin',(128.273548427401,255.,37.9151793916432));
#28048=CARTESIAN_POINT('',(128.273548427401,216.,39.4187321117283));
#28049=CARTESIAN_POINT('',(128.273548427401,255.,39.4187321117283));
#28050=CARTESIAN_POINT('',(128.273548427401,216.,39.4187321117283));
#28051=CARTESIAN_POINT('Origin',(127.637659789347,255.,47.5000804575095));
#28052=CARTESIAN_POINT('',(127.637659789347,216.,47.5000804575095));
#28053=CARTESIAN_POINT('',(142.094409841973,216.,47.5000804575095));
#28054=CARTESIAN_POINT('',(127.637659789347,255.,47.5000804575095));
#28055=CARTESIAN_POINT('Origin',(127.149786002621,255.,47.007169160326));
#28056=CARTESIAN_POINT('',(127.149786002621,216.,47.007169160326));
#28057=CARTESIAN_POINT('',(127.637659789347,216.,47.5000804575095));
#28058=CARTESIAN_POINT('',(127.149786002621,255.,47.007169160326));
#28059=CARTESIAN_POINT('Origin',(127.469614165074,255.,46.690609613792));
#28060=CARTESIAN_POINT('',(127.036092546462,216.,46.8112703207193));
#28061=CARTESIAN_POINT('Origin',(127.469614165074,216.,46.690609613792));
#28062=CARTESIAN_POINT('',(127.036092546462,255.,46.8112703207193));
#28063=CARTESIAN_POINT('Origin',(124.659008759128,255.,47.4728765656934));
#28064=CARTESIAN_POINT('',(125.387243744723,216.,45.1153516005764));
#28065=CARTESIAN_POINT('Origin',(124.659008759128,216.,47.4728765656934));
#28066=CARTESIAN_POINT('',(125.387243744723,255.,45.1153516005764));
#28067=CARTESIAN_POINT('Origin',(125.601218876064,255.,44.4226470147914));
#28068=CARTESIAN_POINT('',(124.876218876064,216.,44.4226470147914));
#28069=CARTESIAN_POINT('Origin',(125.601218876064,216.,44.4226470147914));
#28070=CARTESIAN_POINT('',(124.876218876064,255.,44.4226470147914));
#28071=CARTESIAN_POINT('Origin',(124.876218876064,255.,43.5036225521864));
#28072=CARTESIAN_POINT('',(124.876218876064,216.,43.5036225521864));
#28073=CARTESIAN_POINT('',(124.876218876064,216.,44.4226470147914));
#28074=CARTESIAN_POINT('',(124.876218876064,255.,43.5036225521864));
#28075=CARTESIAN_POINT('Origin',(125.476218876064,255.,43.5036225521863));
#28076=CARTESIAN_POINT('',(125.328762843953,216.,42.9220241352404));
#28077=CARTESIAN_POINT('Origin',(125.476218876064,216.,43.5036225521863));
#28078=CARTESIAN_POINT('',(125.328762843953,255.,42.9220241352404));
#28079=CARTESIAN_POINT('Origin',(124.747780443448,255.,40.6305041508116));
#28080=CARTESIAN_POINT('',(126.997701127708,216.,41.3560806824536));
#28081=CARTESIAN_POINT('Origin',(124.747780443448,216.,40.6305041508116));
#28082=CARTESIAN_POINT('',(126.997701127708,255.,41.3560806824536));
#28083=CARTESIAN_POINT('Origin',(128.330128544122,255.,41.785774969114));
#28084=CARTESIAN_POINT('',(127.333356762198,216.,40.8026951072716));
#28085=CARTESIAN_POINT('Origin',(128.330128544122,216.,41.785774969114));
#28086=CARTESIAN_POINT('',(127.333356762198,255.,40.8026951072716));
#28087=CARTESIAN_POINT('Origin',(127.971127263844,255.,40.1560420081102));
#28088=CARTESIAN_POINT('',(127.971127263844,216.,40.1560420081102));
#28089=CARTESIAN_POINT('',(127.333356762198,216.,40.8026951072716));
#28090=CARTESIAN_POINT('',(127.971127263844,255.,40.1560420081102));
#28091=CARTESIAN_POINT('Origin',(127.223548427401,255.,39.4187321117283));
#28092=CARTESIAN_POINT('Origin',(127.223548427401,216.,39.4187321117283));
#28093=CARTESIAN_POINT('Origin',(134.86603481566,216.,46.7971431424625));
#28094=CARTESIAN_POINT('Origin',(142.094409841973,255.,47.5000804575095));
#28095=CARTESIAN_POINT('',(142.094409841973,230.,47.5000804575095));
#28096=CARTESIAN_POINT('',(142.5822836287,230.,47.007169160326));
#28097=CARTESIAN_POINT('',(144.48829315277,230.,45.0814792533986));
#28098=CARTESIAN_POINT('',(142.094409841973,280.,47.5000804575095));
#28099=CARTESIAN_POINT('',(142.094409841973,255.,47.5000804575095));
#28100=CARTESIAN_POINT('',(142.5822836287,280.,47.007169160326));
#28101=CARTESIAN_POINT('',(144.655606318974,280.,44.9124385054979));
#28102=CARTESIAN_POINT('',(142.5822836287,255.,47.007169160326));
#28103=CARTESIAN_POINT('Origin',(142.262455466246,255.,46.690609613792));
#28104=CARTESIAN_POINT('',(142.695977084858,230.,46.8112703207193));
#28105=CARTESIAN_POINT('Origin',(142.262455466246,230.,46.690609613792));
#28106=CARTESIAN_POINT('',(142.695977084858,280.,46.8112703207193));
#28107=CARTESIAN_POINT('Origin',(142.262455466246,280.,46.690609613792));
#28108=CARTESIAN_POINT('',(142.695977084858,255.,46.8112703207193));
#28109=CARTESIAN_POINT('Origin',(145.073060872192,255.,47.4728765656934));
#28110=CARTESIAN_POINT('',(144.344825886597,230.,45.1153516005764));
#28111=CARTESIAN_POINT('Origin',(145.073060872192,230.,47.4728765656934));
#28112=CARTESIAN_POINT('',(144.344825886597,280.,45.1153516005764));
#28113=CARTESIAN_POINT('Origin',(145.073060872192,280.,47.4728765656934));
#28114=CARTESIAN_POINT('',(144.344825886597,255.,45.1153516005764));
#28115=CARTESIAN_POINT('Origin',(144.130850755256,255.,44.4226470147914));
#28116=CARTESIAN_POINT('',(144.855850755256,230.,44.4226470147914));
#28117=CARTESIAN_POINT('Origin',(144.130850755256,230.,44.4226470147914));
#28118=CARTESIAN_POINT('',(144.855850755256,280.,44.4226470147914));
#28119=CARTESIAN_POINT('Origin',(144.130850755256,280.,44.4226470147914));
#28120=CARTESIAN_POINT('',(144.855850755256,255.,44.4226470147914));
#28121=CARTESIAN_POINT('Origin',(144.855850755256,255.,44.4226470147914));
#28122=CARTESIAN_POINT('',(144.855850755256,230.,43.5036225521863));
#28123=CARTESIAN_POINT('',(144.855850755256,230.,22.2113235073957));
#28124=CARTESIAN_POINT('',(144.855850755256,280.,43.5036225521863));
#28125=CARTESIAN_POINT('',(144.855850755256,280.,22.2113235073957));
#28126=CARTESIAN_POINT('',(144.855850755256,255.,43.5036225521863));
#28127=CARTESIAN_POINT('Origin',(144.255850755256,255.,43.5036225521863));
#28128=CARTESIAN_POINT('',(144.403306787367,230.,42.9220241352404));
#28129=CARTESIAN_POINT('Origin',(144.255850755256,230.,43.5036225521863));
#28130=CARTESIAN_POINT('',(144.403306787367,280.,42.9220241352404));
#28131=CARTESIAN_POINT('Origin',(144.255850755256,280.,43.5036225521863));
#28132=CARTESIAN_POINT('',(144.403306787367,255.,42.9220241352404));
#28133=CARTESIAN_POINT('Origin',(144.984289187872,255.,40.6305041508117));
#28134=CARTESIAN_POINT('',(142.734368503612,230.,41.3560806824536));
#28135=CARTESIAN_POINT('Origin',(144.984289187872,230.,40.6305041508117));
#28136=CARTESIAN_POINT('',(142.734368503612,280.,41.3560806824536));
#28137=CARTESIAN_POINT('Origin',(144.984289187872,280.,40.6305041508117));
#28138=CARTESIAN_POINT('',(142.734368503612,255.,41.3560806824536));
#28139=CARTESIAN_POINT('Origin',(145.869719034433,230.,53.247581206998));
#28140=CARTESIAN_POINT('',(156.375609963127,230.,46.4955106076453));
#28141=CARTESIAN_POINT('',(156.873403253207,230.,46.9933038977248));
#28142=CARTESIAN_POINT('',(156.373403253207,230.,46.4933038977248));
#28143=CARTESIAN_POINT('',(156.873403253207,230.,58.9996518063507));
#28144=CARTESIAN_POINT('',(156.873403253207,230.,46.9933038977248));
#28145=CARTESIAN_POINT('',(155.873403253207,230.,59.9996518063507));
#28146=CARTESIAN_POINT('',(156.873403253207,230.,58.9996518063507));
#28147=CARTESIAN_POINT('',(146.869163947974,230.,59.9996518063508));
#28148=CARTESIAN_POINT('',(155.873403253207,230.,59.9996518063507));
#28149=CARTESIAN_POINT('',(145.466250243448,230.,59.4840979918677));
#28150=CARTESIAN_POINT('Origin',(145.466250243448,230.,61.6506638626042));
#28151=CARTESIAN_POINT('',(124.265819387872,230.,59.4840979918677));
#28152=CARTESIAN_POINT('',(145.466250243448,230.,59.4840979918677));
#28153=CARTESIAN_POINT('',(122.862905683347,230.,59.9996518063507));
#28154=CARTESIAN_POINT('Origin',(124.265819387872,230.,61.6506638626042));
#28155=CARTESIAN_POINT('',(113.858666378113,230.,59.9996518063507));
#28156=CARTESIAN_POINT('',(113.858666378113,230.,59.9996518063507));
#28157=CARTESIAN_POINT('',(112.858666378113,230.,58.9996518063507));
#28158=CARTESIAN_POINT('',(112.858666378113,230.,58.9996518063507));
#28159=CARTESIAN_POINT('',(112.858666378114,230.,46.9933038977248));
#28160=CARTESIAN_POINT('',(112.858666378114,230.,46.9933038977248));
#28161=CARTESIAN_POINT('',(113.356459668193,230.,46.4955106076453));
#28162=CARTESIAN_POINT('',(113.358666378114,230.,46.4933038977248));
#28163=CARTESIAN_POINT('',(113.356459668193,230.,36.0032237681315));
#28164=CARTESIAN_POINT('',(113.356459668193,230.,29.0455312583968));
#28165=CARTESIAN_POINT('',(114.856459668193,230.,34.5032237681315));
#28166=CARTESIAN_POINT('',(119.962847072938,230.,29.3968363633866));
#28167=CARTESIAN_POINT('',(125.314401519217,230.,34.5032237681315));
#28168=CARTESIAN_POINT('',(109.317622593617,230.,34.5032237681315));
#28169=CARTESIAN_POINT('',(127.968500624638,230.,37.1752157277839));
#28170=CARTESIAN_POINT('',(111.34106001963,230.,20.435679696352));
#28171=CARTESIAN_POINT('',(128.273548427401,230.,37.9151793916432));
#28172=CARTESIAN_POINT('Origin',(127.223548427401,230.,37.9151793916432));
#28173=CARTESIAN_POINT('',(128.273548427401,230.,39.4187321117283));
#28174=CARTESIAN_POINT('',(128.273548427401,230.,18.9575896958216));
#28175=CARTESIAN_POINT('',(127.971127263844,230.,40.1560420081102));
#28176=CARTESIAN_POINT('Origin',(127.223548427401,230.,39.4187321117283));
#28177=CARTESIAN_POINT('',(127.333356762198,230.,40.8026951072716));
#28178=CARTESIAN_POINT('',(132.044740758987,230.,36.025692948968));
#28179=CARTESIAN_POINT('',(126.997701127708,230.,41.3560806824536));
#28180=CARTESIAN_POINT('Origin',(128.330128544122,230.,41.785774969114));
#28181=CARTESIAN_POINT('',(125.328762843953,230.,42.9220241352404));
#28182=CARTESIAN_POINT('Origin',(124.747780443448,230.,40.6305041508116));
#28183=CARTESIAN_POINT('',(124.876218876064,230.,43.5036225521864));
#28184=CARTESIAN_POINT('Origin',(125.476218876064,230.,43.5036225521863));
#28185=CARTESIAN_POINT('',(124.876218876064,230.,44.4226470147914));
#28186=CARTESIAN_POINT('',(124.876218876064,230.,21.751811276093));
#28187=CARTESIAN_POINT('',(125.387243744723,230.,45.1153516005764));
#28188=CARTESIAN_POINT('Origin',(125.601218876064,230.,44.4226470147914));
#28189=CARTESIAN_POINT('',(127.036092546462,230.,46.8112703207193));
#28190=CARTESIAN_POINT('Origin',(124.659008759128,230.,47.4728765656934));
#28191=CARTESIAN_POINT('',(127.149786002621,230.,47.007169160326));
#28192=CARTESIAN_POINT('Origin',(127.469614165074,230.,46.690609613792));
#28193=CARTESIAN_POINT('',(127.637659789347,230.,47.5000804575095));
#28194=CARTESIAN_POINT('',(109.61588112148,230.,29.2922190342974));
#28195=CARTESIAN_POINT('',(115.708222654194,230.,47.5000804575095));
#28196=CARTESIAN_POINT('',(142.398712869122,230.,40.8026951072716));
#28197=CARTESIAN_POINT('Origin',(141.401941087198,230.,41.7857749691141));
#28198=CARTESIAN_POINT('',(141.760942367476,230.,40.1560420081102));
#28199=CARTESIAN_POINT('',(122.677567086127,230.,20.8068815557118));
#28200=CARTESIAN_POINT('',(141.458521203919,230.,39.4187321117283));
#28201=CARTESIAN_POINT('Origin',(142.508521203919,230.,39.4187321117283));
#28202=CARTESIAN_POINT('',(141.458521203919,230.,37.9151793916432));
#28203=CARTESIAN_POINT('',(141.45852120392,230.,19.7093660558644));
#28204=CARTESIAN_POINT('',(141.763569006683,230.,37.1752157277839));
#28205=CARTESIAN_POINT('Origin',(142.508521203919,230.,37.9151793916432));
#28206=CARTESIAN_POINT('',(144.417668112103,230.,34.5032237681314));
#28207=CARTESIAN_POINT('',(141.62477097808,230.,37.3149494761148));
#28208=CARTESIAN_POINT('',(154.875609963127,230.,34.5032237681314));
#28209=CARTESIAN_POINT('',(124.098226815572,230.,34.5032237681314));
#28210=CARTESIAN_POINT('',(156.375609963127,230.,36.0032237681314));
#28211=CARTESIAN_POINT('',(133.475597910073,230.,13.1032117150771));
#28212=CARTESIAN_POINT('',(156.375609963127,230.,18.0016118840657));
#28213=CARTESIAN_POINT('Origin',(156.375609963127,255.,46.4955106076453));
#28214=CARTESIAN_POINT('',(156.873403253207,280.,46.9933038977248));
#28215=CARTESIAN_POINT('',(156.873403253207,255.,46.9933038977248));
#28216=CARTESIAN_POINT('',(156.375609963127,280.,46.4955106076453));
#28217=CARTESIAN_POINT('',(156.375609963127,255.,46.4955106076453));
#28218=CARTESIAN_POINT('',(156.373403253207,280.,46.4933038977248));
#28219=CARTESIAN_POINT('Origin',(156.873403253207,255.,46.9933038977248));
#28220=CARTESIAN_POINT('',(156.873403253207,280.,58.9996518063507));
#28221=CARTESIAN_POINT('',(156.873403253207,255.,58.9996518063507));
#28222=CARTESIAN_POINT('',(156.873403253207,280.,46.9933038977248));
#28223=CARTESIAN_POINT('Origin',(156.873403253207,255.,58.9996518063507));
#28224=CARTESIAN_POINT('',(155.873403253207,280.,59.9996518063507));
#28225=CARTESIAN_POINT('',(155.873403253207,255.,59.9996518063507));
#28226=CARTESIAN_POINT('',(156.873403253207,280.,58.9996518063507));
#28227=CARTESIAN_POINT('Origin',(155.873403253207,255.,59.9996518063507));
#28228=CARTESIAN_POINT('',(146.869163947974,280.,59.9996518063508));
#28229=CARTESIAN_POINT('',(146.869163947974,255.,59.9996518063508));
#28230=CARTESIAN_POINT('',(155.873403253207,280.,59.9996518063507));
#28231=CARTESIAN_POINT('',(154.37128360059,270.562970493524,59.9996518063507));
#28232=CARTESIAN_POINT('Origin',(151.37128360059,270.562970493524,59.9996518063507));
#28233=CARTESIAN_POINT('',(154.37128360059,238.562970493524,59.9996518063507));
#28234=CARTESIAN_POINT('Origin',(151.37128360059,238.562970493524,59.9996518063507));
#28235=CARTESIAN_POINT('Origin',(145.466250243448,255.,61.6506638626042));
#28236=CARTESIAN_POINT('',(145.466250243448,280.,59.4840979918677));
#28237=CARTESIAN_POINT('',(145.466250243448,255.,59.4840979918677));
#28238=CARTESIAN_POINT('Origin',(145.466250243448,280.,61.6506638626042));
#28239=CARTESIAN_POINT('Origin',(145.466250243448,255.,59.4840979918677));
#28240=CARTESIAN_POINT('',(124.265819387872,280.,59.4840979918677));
#28241=CARTESIAN_POINT('',(124.265819387872,280.,59.4840979918677));
#28242=CARTESIAN_POINT('',(124.265819387872,255.,59.4840979918677));
#28243=CARTESIAN_POINT('Origin',(145.869719034433,280.,53.247581206998));
#28244=CARTESIAN_POINT('',(156.375609963127,280.,36.0032237681314));
#28245=CARTESIAN_POINT('',(156.375609963127,280.,18.0016118840657));
#28246=CARTESIAN_POINT('',(154.875609963127,280.,34.5032237681314));
#28247=CARTESIAN_POINT('',(133.644647576992,280.,13.2722613819965));
#28248=CARTESIAN_POINT('',(144.417668112103,280.,34.5032237681314));
#28249=CARTESIAN_POINT('',(124.436326149411,280.,34.5032237681314));
#28250=CARTESIAN_POINT('',(141.763569006683,280.,37.1752157277839));
#28251=CARTESIAN_POINT('',(141.792684822546,280.,37.1459036249592));
#28252=CARTESIAN_POINT('',(141.458521203919,280.,37.9151793916432));
#28253=CARTESIAN_POINT('Origin',(142.508521203919,280.,37.9151793916432));
#28254=CARTESIAN_POINT('',(141.458521203919,280.,39.4187321117283));
#28255=CARTESIAN_POINT('',(141.45852120392,280.,19.7093660558643));
#28256=CARTESIAN_POINT('',(141.760942367476,280.,40.1560420081102));
#28257=CARTESIAN_POINT('Origin',(142.508521203919,280.,39.4187321117283));
#28258=CARTESIAN_POINT('',(142.398712869122,280.,40.8026951072716));
#28259=CARTESIAN_POINT('',(122.844278695199,280.,20.9759150534898));
#28260=CARTESIAN_POINT('Origin',(141.401941087198,280.,41.7857749691141));
#28261=CARTESIAN_POINT('',(127.637659789347,280.,47.5000804575095));
#28262=CARTESIAN_POINT('',(116.046321988033,280.,47.5000804575095));
#28263=CARTESIAN_POINT('',(127.149786002621,280.,47.007169160326));
#28264=CARTESIAN_POINT('',(109.783194287684,280.,29.4612597821981));
#28265=CARTESIAN_POINT('',(127.036092546462,280.,46.8112703207193));
#28266=CARTESIAN_POINT('Origin',(127.469614165074,280.,46.690609613792));
#28267=CARTESIAN_POINT('',(125.387243744723,280.,45.1153516005764));
#28268=CARTESIAN_POINT('Origin',(124.659008759128,280.,47.4728765656934));
#28269=CARTESIAN_POINT('',(124.876218876064,280.,44.4226470147914));
#28270=CARTESIAN_POINT('Origin',(125.601218876064,280.,44.4226470147914));
#28271=CARTESIAN_POINT('',(124.876218876064,280.,43.5036225521864));
#28272=CARTESIAN_POINT('',(124.876218876064,280.,21.751811276093));
#28273=CARTESIAN_POINT('',(125.328762843953,280.,42.9220241352404));
#28274=CARTESIAN_POINT('Origin',(125.476218876064,280.,43.5036225521863));
#28275=CARTESIAN_POINT('',(126.997701127708,280.,41.3560806824536));
#28276=CARTESIAN_POINT('Origin',(124.747780443448,280.,40.6305041508116));
#28277=CARTESIAN_POINT('',(127.333356762198,280.,40.8026951072716));
#28278=CARTESIAN_POINT('Origin',(128.330128544122,280.,41.785774969114));
#28279=CARTESIAN_POINT('',(127.971127263844,280.,40.1560420081102));
#28280=CARTESIAN_POINT('',(132.211452368059,280.,35.85665945119));
#28281=CARTESIAN_POINT('',(128.273548427401,280.,39.4187321117283));
#28282=CARTESIAN_POINT('Origin',(127.223548427401,280.,39.4187321117283));
#28283=CARTESIAN_POINT('',(128.273548427401,280.,37.9151793916432));
#28284=CARTESIAN_POINT('',(128.273548427401,280.,18.9575896958216));
#28285=CARTESIAN_POINT('',(127.968500624638,280.,37.1752157277839));
#28286=CARTESIAN_POINT('Origin',(127.223548427401,280.,37.9151793916432));
#28287=CARTESIAN_POINT('',(125.314401519217,280.,34.5032237681315));
#28288=CARTESIAN_POINT('',(111.508973864096,280.,20.6047255475076));
#28289=CARTESIAN_POINT('',(114.856459668193,280.,34.5032237681315));
#28290=CARTESIAN_POINT('',(109.655721927456,280.,34.5032237681315));
#28291=CARTESIAN_POINT('',(113.356459668193,280.,36.0032237681315));
#28292=CARTESIAN_POINT('',(120.131896739857,280.,29.2277866964671));
#28293=CARTESIAN_POINT('',(113.356459668193,280.,46.4955106076453));
#28294=CARTESIAN_POINT('',(113.356459668193,280.,29.0455312583968));
#28295=CARTESIAN_POINT('',(112.858666378114,280.,46.9933038977248));
#28296=CARTESIAN_POINT('',(113.358666378114,280.,46.4933038977248));
#28297=CARTESIAN_POINT('',(112.858666378113,280.,58.9996518063507));
#28298=CARTESIAN_POINT('',(112.858666378114,280.,46.9933038977248));
#28299=CARTESIAN_POINT('',(113.858666378113,280.,59.9996518063507));
#28300=CARTESIAN_POINT('',(112.858666378113,280.,58.9996518063507));
#28301=CARTESIAN_POINT('',(122.862905683347,280.,59.9996518063507));
#28302=CARTESIAN_POINT('',(113.858666378113,280.,59.9996518063507));
#28303=CARTESIAN_POINT('Origin',(124.265819387872,280.,61.6506638626042));
#28304=CARTESIAN_POINT('Origin',(113.356459668193,255.,46.4955106076453));
#28305=CARTESIAN_POINT('',(112.858666378114,255.,46.9933038977248));
#28306=CARTESIAN_POINT('',(113.356459668193,255.,46.4955106076453));
#28307=CARTESIAN_POINT('Origin',(112.858666378114,255.,46.9933038977248));
#28308=CARTESIAN_POINT('',(112.858666378113,255.,58.9996518063507));
#28309=CARTESIAN_POINT('Origin',(112.858666378113,255.,58.9996518063507));
#28310=CARTESIAN_POINT('',(113.858666378113,255.,59.9996518063507));
#28311=CARTESIAN_POINT('Origin',(113.858666378113,255.,59.9996518063507));
#28312=CARTESIAN_POINT('',(122.862905683347,255.,59.9996518063507));
#28313=CARTESIAN_POINT('',(121.37128360059,270.562970493524,59.9996518063507));
#28314=CARTESIAN_POINT('Origin',(118.37128360059,270.562970493524,59.9996518063507));
#28315=CARTESIAN_POINT('',(121.37128360059,238.562970493524,59.9996518063507));
#28316=CARTESIAN_POINT('Origin',(118.37128360059,238.562970493524,59.9996518063507));
#28317=CARTESIAN_POINT('Origin',(124.265819387872,255.,61.6506638626042));
#28318=CARTESIAN_POINT('Origin',(151.37128360059,238.562970493524,59.9996518063507));
#28319=CARTESIAN_POINT('',(154.37128360059,238.562970493524,34.5032237681314));
#28320=CARTESIAN_POINT('',(154.37128360059,238.562970493524,59.9996518063507));
#28321=CARTESIAN_POINT('Origin',(151.37128360059,238.562970493524,34.5032237681314));
#28322=CARTESIAN_POINT('Origin',(118.37128360059,238.562970493524,59.9996518063507));
#28323=CARTESIAN_POINT('',(121.37128360059,238.562970493524,34.5032237681315));
#28324=CARTESIAN_POINT('',(121.37128360059,238.562970493524,59.9996518063507));
#28325=CARTESIAN_POINT('Origin',(118.37128360059,238.562970493524,34.5032237681315));
#28326=CARTESIAN_POINT('Origin',(151.37128360059,270.562970493524,59.9996518063507));
#28327=CARTESIAN_POINT('',(154.37128360059,270.562970493524,34.5032237681314));
#28328=CARTESIAN_POINT('',(154.37128360059,270.562970493524,59.9996518063507));
#28329=CARTESIAN_POINT('Origin',(151.37128360059,270.562970493524,34.5032237681314));
#28330=CARTESIAN_POINT('Origin',(118.37128360059,270.562970493524,59.9996518063507));
#28331=CARTESIAN_POINT('',(121.37128360059,270.562970493524,34.5032237681315));
#28332=CARTESIAN_POINT('',(121.37128360059,270.562970493524,59.9996518063507));
#28333=CARTESIAN_POINT('Origin',(118.37128360059,270.562970493524,34.5032237681315));
#28334=CARTESIAN_POINT('Origin',(156.375609963127,255.,36.0032237681314));
#28335=CARTESIAN_POINT('',(156.375609963127,255.,36.0032237681314));
#28336=CARTESIAN_POINT('Origin',(154.875609963127,255.,34.5032237681314));
#28337=CARTESIAN_POINT('',(154.875609963127,255.,34.5032237681314));
#28338=CARTESIAN_POINT('Origin',(144.417668112103,255.,34.5032237681314));
#28339=CARTESIAN_POINT('',(144.417668112103,255.,34.5032237681314));
#28340=CARTESIAN_POINT('Origin',(141.763569006683,255.,37.1752157277839));
#28341=CARTESIAN_POINT('',(141.763569006683,255.,37.1752157277839));
#28342=CARTESIAN_POINT('Origin',(142.508521203919,255.,37.9151793916432));
#28343=CARTESIAN_POINT('',(141.458521203919,255.,37.9151793916432));
#28344=CARTESIAN_POINT('Origin',(141.458521203919,255.,39.4187321117283));
#28345=CARTESIAN_POINT('',(141.458521203919,255.,39.4187321117283));
#28346=CARTESIAN_POINT('Origin',(142.508521203919,255.,39.4187321117283));
#28347=CARTESIAN_POINT('',(141.760942367476,255.,40.1560420081102));
#28348=CARTESIAN_POINT('Origin',(142.398712869122,255.,40.8026951072716));
#28349=CARTESIAN_POINT('',(142.398712869122,255.,40.8026951072716));
#28350=CARTESIAN_POINT('Origin',(141.401941087198,255.,41.7857749691141));
#28351=CARTESIAN_POINT('Origin',(113.356459668193,255.,58.0910625167937));
#28352=CARTESIAN_POINT('',(113.356459668193,255.,36.0032237681315));
#28353=CARTESIAN_POINT('Origin',(113.356459668193,255.,36.0032237681315));
#28354=CARTESIAN_POINT('',(114.856459668193,255.,34.5032237681315));
#28355=CARTESIAN_POINT('Origin',(114.856459668193,255.,34.5032237681315));
#28356=CARTESIAN_POINT('',(125.314401519217,255.,34.5032237681315));
#28357=CARTESIAN_POINT('Origin',(125.314401519217,255.,34.5032237681315));
#28358=CARTESIAN_POINT('',(127.968500624638,255.,37.1752157277839));
#28359=CARTESIAN_POINT('Origin',(127.223548427401,255.,37.9151793916432));
#28360=CARTESIAN_POINT('',(128.273548427401,255.,37.9151793916432));
#28361=CARTESIAN_POINT('Origin',(128.273548427401,255.,37.9151793916432));
#28362=CARTESIAN_POINT('',(128.273548427401,255.,39.4187321117283));
#28363=CARTESIAN_POINT('Origin',(127.223548427401,255.,39.4187321117283));
#28364=CARTESIAN_POINT('',(127.971127263844,255.,40.1560420081102));
#28365=CARTESIAN_POINT('Origin',(127.971127263844,255.,40.1560420081102));
#28366=CARTESIAN_POINT('',(127.333356762198,255.,40.8026951072716));
#28367=CARTESIAN_POINT('Origin',(128.330128544122,255.,41.785774969114));
#28368=CARTESIAN_POINT('',(126.997701127708,255.,41.3560806824536));
#28369=CARTESIAN_POINT('Origin',(124.747780443448,255.,40.6305041508116));
#28370=CARTESIAN_POINT('',(125.328762843953,255.,42.9220241352404));
#28371=CARTESIAN_POINT('Origin',(125.476218876064,255.,43.5036225521863));
#28372=CARTESIAN_POINT('',(124.876218876064,255.,43.5036225521864));
#28373=CARTESIAN_POINT('Origin',(124.876218876064,255.,43.5036225521864));
#28374=CARTESIAN_POINT('',(124.876218876064,255.,44.4226470147914));
#28375=CARTESIAN_POINT('Origin',(125.601218876064,255.,44.4226470147914));
#28376=CARTESIAN_POINT('',(125.387243744723,255.,45.1153516005764));
#28377=CARTESIAN_POINT('Origin',(124.659008759128,255.,47.4728765656934));
#28378=CARTESIAN_POINT('',(127.036092546462,255.,46.8112703207193));
#28379=CARTESIAN_POINT('Origin',(127.469614165074,255.,46.690609613792));
#28380=CARTESIAN_POINT('',(127.149786002621,255.,47.007169160326));
#28381=CARTESIAN_POINT('Origin',(127.149786002621,255.,47.007169160326));
#28382=CARTESIAN_POINT('',(127.637659789347,255.,47.5000804575095));
#28383=CARTESIAN_POINT('Origin',(127.637659789347,255.,47.5000804575095));
#28384=CARTESIAN_POINT('Origin',(141.401941087198,255.,41.7857749691141));
#28385=CARTESIAN_POINT('',(142.734368503612,280.,41.3560806824536));
#28386=CARTESIAN_POINT('',(142.398712869122,280.,40.8026951072716));
#28387=CARTESIAN_POINT('Origin',(141.401941087198,280.,41.7857749691141));
#28388=CARTESIAN_POINT('',(142.734368503612,294.,41.3560806824536));
#28389=CARTESIAN_POINT('',(142.734368503612,255.,41.3560806824536));
#28390=CARTESIAN_POINT('',(142.398712869122,294.,40.8026951072716));
#28391=CARTESIAN_POINT('Origin',(141.401941087198,294.,41.7857749691141));
#28392=CARTESIAN_POINT('',(142.398712869122,255.,40.8026951072716));
#28393=CARTESIAN_POINT('Origin',(142.398712869122,255.,40.8026951072716));
#28394=CARTESIAN_POINT('',(141.760942367476,280.,40.1560420081102));
#28395=CARTESIAN_POINT('',(122.844278695199,280.,20.9759150534898));
#28396=CARTESIAN_POINT('',(141.760942367476,294.,40.1560420081102));
#28397=CARTESIAN_POINT('',(141.760942367476,294.,40.1560420081102));
#28398=CARTESIAN_POINT('',(141.760942367476,255.,40.1560420081102));
#28399=CARTESIAN_POINT('Origin',(142.508521203919,255.,39.4187321117283));
#28400=CARTESIAN_POINT('',(141.458521203919,280.,39.4187321117283));
#28401=CARTESIAN_POINT('Origin',(142.508521203919,280.,39.4187321117283));
#28402=CARTESIAN_POINT('',(141.458521203919,294.,39.4187321117283));
#28403=CARTESIAN_POINT('Origin',(142.508521203919,294.,39.4187321117283));
#28404=CARTESIAN_POINT('',(141.458521203919,255.,39.4187321117283));
#28405=CARTESIAN_POINT('Origin',(141.458521203919,255.,39.4187321117283));
#28406=CARTESIAN_POINT('',(141.458521203919,280.,37.9151793916432));
#28407=CARTESIAN_POINT('',(141.45852120392,280.,19.7093660558643));
#28408=CARTESIAN_POINT('',(141.458521203919,294.,37.9151793916432));
#28409=CARTESIAN_POINT('',(141.458521203919,294.,37.9151793916432));
#28410=CARTESIAN_POINT('',(141.458521203919,255.,37.9151793916432));
#28411=CARTESIAN_POINT('Origin',(142.508521203919,255.,37.9151793916432));
#28412=CARTESIAN_POINT('',(141.763569006683,280.,37.1752157277839));
#28413=CARTESIAN_POINT('Origin',(142.508521203919,280.,37.9151793916432));
#28414=CARTESIAN_POINT('',(141.763569006683,294.,37.1752157277839));
#28415=CARTESIAN_POINT('Origin',(142.508521203919,294.,37.9151793916432));
#28416=CARTESIAN_POINT('',(141.763569006683,255.,37.1752157277839));
#28417=CARTESIAN_POINT('Origin',(141.763569006683,255.,37.1752157277839));
#28418=CARTESIAN_POINT('',(144.417668112103,280.,34.5032237681314));
#28419=CARTESIAN_POINT('',(141.792684822546,280.,37.1459036249592));
#28420=CARTESIAN_POINT('',(144.417668112103,294.,34.5032237681314));
#28421=CARTESIAN_POINT('',(144.544688744748,294.,34.375346814161));
#28422=CARTESIAN_POINT('',(144.417668112103,255.,34.5032237681314));
#28423=CARTESIAN_POINT('Origin',(144.417668112103,255.,34.5032237681314));
#28424=CARTESIAN_POINT('',(154.875609963127,280.,34.5032237681314));
#28425=CARTESIAN_POINT('',(124.436326149411,280.,34.5032237681314));
#28426=CARTESIAN_POINT('',(154.875609963127,294.,34.5032237681314));
#28427=CARTESIAN_POINT('',(134.86603481566,294.,34.5032237681314));
#28428=CARTESIAN_POINT('',(154.875609963127,255.,34.5032237681314));
#28429=CARTESIAN_POINT('Origin',(154.875609963127,255.,34.5032237681314));
#28430=CARTESIAN_POINT('',(156.375609963127,280.,36.0032237681314));
#28431=CARTESIAN_POINT('',(133.644647576992,280.,13.2722613819965));
#28432=CARTESIAN_POINT('',(156.375609963127,294.,36.0032237681314));
#28433=CARTESIAN_POINT('',(154.875609963127,294.,34.5032237681314));
#28434=CARTESIAN_POINT('',(156.375609963127,255.,36.0032237681314));
#28435=CARTESIAN_POINT('Origin',(156.375609963127,255.,58.0910625167936));
#28436=CARTESIAN_POINT('',(155.375609963127,280.,59.0910625167936));
#28437=CARTESIAN_POINT('',(156.375609963127,280.,58.0910625167936));
#28438=CARTESIAN_POINT('',(154.960007558403,280.,59.5066649215182));
#28439=CARTESIAN_POINT('',(156.375609963127,294.,58.0910625167936));
#28440=CARTESIAN_POINT('',(156.375609963127,255.,58.0910625167936));
#28441=CARTESIAN_POINT('',(155.375609963127,294.,59.0910625167936));
#28442=CARTESIAN_POINT('',(156.375609963127,294.,58.0910625167936));
#28443=CARTESIAN_POINT('',(155.375609963127,255.,59.0910625167936));
#28444=CARTESIAN_POINT('Origin',(155.375609963127,255.,59.0910625167936));
#28445=CARTESIAN_POINT('',(114.356459668193,280.,59.0910625167936));
#28446=CARTESIAN_POINT('',(150.62266449878,280.,59.0910625167936));
#28447=CARTESIAN_POINT('',(114.356459668193,294.,59.0910625167936));
#28448=CARTESIAN_POINT('',(155.375609963127,294.,59.0910625167936));
#28449=CARTESIAN_POINT('',(114.356459668193,255.,59.0910625167936));
#28450=CARTESIAN_POINT('Origin',(114.356459668193,255.,59.0910625167936));
#28451=CARTESIAN_POINT('',(113.356459668193,280.,58.0910625167936));
#28452=CARTESIAN_POINT('',(120.773904182304,280.,65.5085070309049));
#28453=CARTESIAN_POINT('',(113.356459668193,294.,58.0910625167937));
#28454=CARTESIAN_POINT('',(113.356459668193,294.,58.0910625167937));
#28455=CARTESIAN_POINT('',(113.356459668193,255.,58.0910625167937));
#28456=CARTESIAN_POINT('Origin',(113.356459668193,255.,58.0910625167937));
#28457=CARTESIAN_POINT('',(113.356459668193,280.,36.0032237681315));
#28458=CARTESIAN_POINT('',(113.356459668193,280.,29.0455312583968));
#28459=CARTESIAN_POINT('',(113.356459668193,294.,36.0032237681315));
#28460=CARTESIAN_POINT('',(113.356459668193,294.,36.0032237681315));
#28461=CARTESIAN_POINT('',(113.356459668193,255.,36.0032237681315));
#28462=CARTESIAN_POINT('Origin',(113.356459668193,255.,36.0032237681315));
#28463=CARTESIAN_POINT('',(114.856459668193,280.,34.5032237681315));
#28464=CARTESIAN_POINT('',(120.131896739857,280.,29.2277866964671));
#28465=CARTESIAN_POINT('',(114.856459668193,294.,34.5032237681315));
#28466=CARTESIAN_POINT('',(114.856459668193,294.,34.5032237681315));
#28467=CARTESIAN_POINT('',(114.856459668193,255.,34.5032237681315));
#28468=CARTESIAN_POINT('Origin',(114.856459668193,255.,34.5032237681315));
#28469=CARTESIAN_POINT('',(125.314401519217,280.,34.5032237681315));
#28470=CARTESIAN_POINT('',(109.655721927456,280.,34.5032237681315));
#28471=CARTESIAN_POINT('',(125.314401519217,294.,34.5032237681315));
#28472=CARTESIAN_POINT('',(134.86603481566,294.,34.5032237681314));
#28473=CARTESIAN_POINT('',(125.314401519217,255.,34.5032237681315));
#28474=CARTESIAN_POINT('Origin',(125.314401519217,255.,34.5032237681315));
#28475=CARTESIAN_POINT('',(127.968500624638,280.,37.1752157277839));
#28476=CARTESIAN_POINT('',(111.508973864096,280.,20.6047255475076));
#28477=CARTESIAN_POINT('',(127.968500624638,294.,37.1752157277839));
#28478=CARTESIAN_POINT('',(127.968500624638,294.,37.1752157277839));
#28479=CARTESIAN_POINT('',(127.968500624638,255.,37.1752157277839));
#28480=CARTESIAN_POINT('Origin',(127.223548427401,255.,37.9151793916432));
#28481=CARTESIAN_POINT('',(128.273548427401,280.,37.9151793916432));
#28482=CARTESIAN_POINT('Origin',(127.223548427401,280.,37.9151793916432));
#28483=CARTESIAN_POINT('',(128.273548427401,294.,37.9151793916432));
#28484=CARTESIAN_POINT('Origin',(127.223548427401,294.,37.9151793916432));
#28485=CARTESIAN_POINT('',(128.273548427401,255.,37.9151793916432));
#28486=CARTESIAN_POINT('Origin',(134.86603481566,294.,46.7971431424625));
#28487=CARTESIAN_POINT('',(127.971127263844,294.,40.1560420081102));
#28488=CARTESIAN_POINT('',(128.273548427401,294.,39.4187321117283));
#28489=CARTESIAN_POINT('Origin',(127.223548427401,294.,39.4187321117283));
#28490=CARTESIAN_POINT('',(128.273548427401,294.,39.4187321117283));
#28491=CARTESIAN_POINT('',(156.375609963127,294.,36.0032237681314));
#28492=CARTESIAN_POINT('',(144.403306787367,294.,42.9220241352404));
#28493=CARTESIAN_POINT('Origin',(144.984289187872,294.,40.6305041508117));
#28494=CARTESIAN_POINT('',(144.855850755256,294.,43.5036225521863));
#28495=CARTESIAN_POINT('Origin',(144.255850755256,294.,43.5036225521863));
#28496=CARTESIAN_POINT('',(144.855850755256,294.,44.4226470147914));
#28497=CARTESIAN_POINT('',(144.855850755256,294.,43.5036225521863));
#28498=CARTESIAN_POINT('',(144.344825886597,294.,45.1153516005764));
#28499=CARTESIAN_POINT('Origin',(144.130850755256,294.,44.4226470147914));
#28500=CARTESIAN_POINT('',(142.695977084858,294.,46.8112703207193));
#28501=CARTESIAN_POINT('Origin',(145.073060872192,294.,47.4728765656934));
#28502=CARTESIAN_POINT('',(142.5822836287,294.,47.007169160326));
#28503=CARTESIAN_POINT('Origin',(142.262455466246,294.,46.690609613792));
#28504=CARTESIAN_POINT('',(142.094409841973,294.,47.5000804575095));
#28505=CARTESIAN_POINT('',(142.5822836287,294.,47.007169160326));
#28506=CARTESIAN_POINT('',(127.637659789347,294.,47.5000804575095));
#28507=CARTESIAN_POINT('',(142.094409841973,294.,47.5000804575095));
#28508=CARTESIAN_POINT('',(127.149786002621,294.,47.007169160326));
#28509=CARTESIAN_POINT('',(127.637659789347,294.,47.5000804575095));
#28510=CARTESIAN_POINT('',(127.036092546462,294.,46.8112703207193));
#28511=CARTESIAN_POINT('Origin',(127.469614165074,294.,46.690609613792));
#28512=CARTESIAN_POINT('',(125.387243744723,294.,45.1153516005764));
#28513=CARTESIAN_POINT('Origin',(124.659008759128,294.,47.4728765656934));
#28514=CARTESIAN_POINT('',(124.876218876064,294.,44.4226470147914));
#28515=CARTESIAN_POINT('Origin',(125.601218876064,294.,44.4226470147914));
#28516=CARTESIAN_POINT('',(124.876218876064,294.,43.5036225521864));
#28517=CARTESIAN_POINT('',(124.876218876064,294.,44.4226470147914));
#28518=CARTESIAN_POINT('',(125.328762843953,294.,42.9220241352404));
#28519=CARTESIAN_POINT('Origin',(125.476218876064,294.,43.5036225521863));
#28520=CARTESIAN_POINT('',(126.997701127708,294.,41.3560806824536));
#28521=CARTESIAN_POINT('Origin',(124.747780443448,294.,40.6305041508116));
#28522=CARTESIAN_POINT('',(127.333356762198,294.,40.8026951072716));
#28523=CARTESIAN_POINT('Origin',(128.330128544122,294.,41.785774969114));
#28524=CARTESIAN_POINT('',(127.333356762198,294.,40.8026951072716));
#28525=CARTESIAN_POINT('Origin',(156.375609963127,255.,36.0032237681314));
#28526=CARTESIAN_POINT('',(156.375609963127,280.,18.0016118840657));
#28527=CARTESIAN_POINT('Origin',(128.273548427401,255.,37.9151793916432));
#28528=CARTESIAN_POINT('',(128.273548427401,280.,39.4187321117283));
#28529=CARTESIAN_POINT('',(128.273548427401,280.,18.9575896958216));
#28530=CARTESIAN_POINT('',(128.273548427401,255.,39.4187321117283));
#28531=CARTESIAN_POINT('Origin',(127.223548427401,255.,39.4187321117283));
#28532=CARTESIAN_POINT('',(127.971127263844,280.,40.1560420081102));
#28533=CARTESIAN_POINT('Origin',(127.223548427401,280.,39.4187321117283));
#28534=CARTESIAN_POINT('',(127.971127263844,255.,40.1560420081102));
#28535=CARTESIAN_POINT('Origin',(127.971127263844,255.,40.1560420081102));
#28536=CARTESIAN_POINT('',(127.333356762198,280.,40.8026951072716));
#28537=CARTESIAN_POINT('',(132.211452368059,280.,35.85665945119));
#28538=CARTESIAN_POINT('',(127.333356762198,255.,40.8026951072716));
#28539=CARTESIAN_POINT('Origin',(128.330128544122,255.,41.785774969114));
#28540=CARTESIAN_POINT('',(126.997701127708,280.,41.3560806824536));
#28541=CARTESIAN_POINT('Origin',(128.330128544122,280.,41.785774969114));
#28542=CARTESIAN_POINT('',(126.997701127708,255.,41.3560806824536));
#28543=CARTESIAN_POINT('Origin',(124.747780443448,255.,40.6305041508116));
#28544=CARTESIAN_POINT('',(125.328762843953,280.,42.9220241352404));
#28545=CARTESIAN_POINT('Origin',(124.747780443448,280.,40.6305041508116));
#28546=CARTESIAN_POINT('',(125.328762843953,255.,42.9220241352404));
#28547=CARTESIAN_POINT('Origin',(125.476218876064,255.,43.5036225521863));
#28548=CARTESIAN_POINT('',(124.876218876064,280.,43.5036225521864));
#28549=CARTESIAN_POINT('Origin',(125.476218876064,280.,43.5036225521863));
#28550=CARTESIAN_POINT('',(124.876218876064,255.,43.5036225521864));
#28551=CARTESIAN_POINT('Origin',(124.876218876064,255.,43.5036225521864));
#28552=CARTESIAN_POINT('',(124.876218876064,280.,44.4226470147914));
#28553=CARTESIAN_POINT('',(124.876218876064,280.,21.751811276093));
#28554=CARTESIAN_POINT('',(124.876218876064,255.,44.4226470147914));
#28555=CARTESIAN_POINT('Origin',(125.601218876064,255.,44.4226470147914));
#28556=CARTESIAN_POINT('',(125.387243744723,280.,45.1153516005764));
#28557=CARTESIAN_POINT('Origin',(125.601218876064,280.,44.4226470147914));
#28558=CARTESIAN_POINT('',(125.387243744723,255.,45.1153516005764));
#28559=CARTESIAN_POINT('Origin',(124.659008759128,255.,47.4728765656934));
#28560=CARTESIAN_POINT('',(127.036092546462,280.,46.8112703207193));
#28561=CARTESIAN_POINT('Origin',(124.659008759128,280.,47.4728765656934));
#28562=CARTESIAN_POINT('',(127.036092546462,255.,46.8112703207193));
#28563=CARTESIAN_POINT('Origin',(127.469614165074,255.,46.690609613792));
#28564=CARTESIAN_POINT('',(127.149786002621,280.,47.007169160326));
#28565=CARTESIAN_POINT('Origin',(127.469614165074,280.,46.690609613792));
#28566=CARTESIAN_POINT('',(127.149786002621,255.,47.007169160326));
#28567=CARTESIAN_POINT('Origin',(127.149786002621,255.,47.007169160326));
#28568=CARTESIAN_POINT('',(127.637659789347,280.,47.5000804575095));
#28569=CARTESIAN_POINT('',(109.783194287684,280.,29.4612597821981));
#28570=CARTESIAN_POINT('',(127.637659789347,255.,47.5000804575095));
#28571=CARTESIAN_POINT('Origin',(127.637659789347,255.,47.5000804575095));
#28572=CARTESIAN_POINT('',(142.094409841973,280.,47.5000804575095));
#28573=CARTESIAN_POINT('',(116.046321988033,280.,47.5000804575095));
#28574=CARTESIAN_POINT('',(142.094409841973,255.,47.5000804575095));
#28575=CARTESIAN_POINT('Origin',(142.094409841973,255.,47.5000804575095));
#28576=CARTESIAN_POINT('',(142.5822836287,280.,47.007169160326));
#28577=CARTESIAN_POINT('',(144.655606318974,280.,44.9124385054979));
#28578=CARTESIAN_POINT('',(142.5822836287,255.,47.007169160326));
#28579=CARTESIAN_POINT('Origin',(142.262455466246,255.,46.690609613792));
#28580=CARTESIAN_POINT('',(142.695977084858,280.,46.8112703207193));
#28581=CARTESIAN_POINT('Origin',(142.262455466246,280.,46.690609613792));
#28582=CARTESIAN_POINT('',(142.695977084858,255.,46.8112703207193));
#28583=CARTESIAN_POINT('Origin',(145.073060872192,255.,47.4728765656934));
#28584=CARTESIAN_POINT('',(144.344825886597,280.,45.1153516005764));
#28585=CARTESIAN_POINT('Origin',(145.073060872192,280.,47.4728765656934));
#28586=CARTESIAN_POINT('',(144.344825886597,255.,45.1153516005764));
#28587=CARTESIAN_POINT('Origin',(144.130850755256,255.,44.4226470147914));
#28588=CARTESIAN_POINT('',(144.855850755256,280.,44.4226470147914));
#28589=CARTESIAN_POINT('Origin',(144.130850755256,280.,44.4226470147914));
#28590=CARTESIAN_POINT('',(144.855850755256,255.,44.4226470147914));
#28591=CARTESIAN_POINT('Origin',(144.855850755256,255.,44.4226470147914));
#28592=CARTESIAN_POINT('',(144.855850755256,280.,43.5036225521863));
#28593=CARTESIAN_POINT('',(144.855850755256,280.,22.2113235073957));
#28594=CARTESIAN_POINT('',(144.855850755256,255.,43.5036225521863));
#28595=CARTESIAN_POINT('Origin',(144.255850755256,255.,43.5036225521863));
#28596=CARTESIAN_POINT('',(144.403306787367,280.,42.9220241352404));
#28597=CARTESIAN_POINT('Origin',(144.255850755256,280.,43.5036225521863));
#28598=CARTESIAN_POINT('',(144.403306787367,255.,42.9220241352404));
#28599=CARTESIAN_POINT('Origin',(144.984289187872,255.,40.6305041508117));
#28600=CARTESIAN_POINT('Origin',(144.984289187872,280.,40.6305041508117));
#28601=CARTESIAN_POINT('Origin',(104.454984186719,280.,0.));
#48346=UNCERTAINTY_MEASURE_WITH_UNIT(LENGTH_MEASURE(0.01),#48370,
'DISTANCE_ACCURACY_VALUE',
'Maximum model space distance between geometric entities at asserted c
onnectivities');
#48356=UNCERTAINTY_MEASURE_WITH_UNIT(LENGTH_MEASURE(0.01),#48370,
'DISTANCE_ACCURACY_VALUE',
'Maximum model space distance between geometric entities at asserted c
onnectivities');
#48359=(
GEOMETRIC_REPRESENTATION_CONTEXT(3)
GLOBAL_UNCERTAINTY_ASSIGNED_CONTEXT((#48346))
GLOBAL_UNIT_ASSIGNED_CONTEXT((#48370,#48372,#48373))
REPRESENTATION_CONTEXT('','3D')
);
#48369=(
GEOMETRIC_REPRESENTATION_CONTEXT(3)
GLOBAL_UNCERTAINTY_ASSIGNED_CONTEXT((#48356))
GLOBAL_UNIT_ASSIGNED_CONTEXT((#48370,#48372,#48373))
REPRESENTATION_CONTEXT('','3D')
);
#48370=(
LENGTH_UNIT()
NAMED_UNIT(*)
SI_UNIT(.MILLI.,.METRE.)
);
#48372=(
NAMED_UNIT(*)
PLANE_ANGLE_UNIT()
SI_UNIT($,.RADIAN.)
);
#48373=(
NAMED_UNIT(*)
SI_UNIT($,.STERADIAN.)
SOLID_ANGLE_UNIT()
);
#48376=SHAPE_DEFINITION_REPRESENTATION(#48388,#48414);
#48388=PRODUCT_DEFINITION_SHAPE('',$,#48427);
#48414=SHAPE_REPRESENTATION('',(#20492),#48359);
#48424=PRODUCT_DEFINITION_CONTEXT('part definition',#48462,'design');
#48427=PRODUCT_DEFINITION('LINEAR GUIDE','LINEAR GUIDE',#48439,#48424);
#48439=PRODUCT_DEFINITION_FORMATION('',$,#48466);
#48462=APPLICATION_CONTEXT(
'Core Data for Automotive Mechanical Design Process');
#48463=PRODUCT_CONTEXT('part definition',#48462,'mechanical');
#48466=PRODUCT('LINEAR GUIDE','LINEAR GUIDE',$,(#48463));
#48525=COLOUR_RGB('Off White',0.89,0.88,0.83);
#48526=FILL_AREA_STYLE_COLOUR('',#48525);
#48527=FILL_AREA_STYLE('',(#48526));
#48528=SURFACE_STYLE_FILL_AREA(#48527);
#48529=SURFACE_SIDE_STYLE('',(#48528));
#48530=SURFACE_STYLE_USAGE(.BOTH.,#48529);
#48531=PRESENTATION_STYLE_ASSIGNMENT((#48530));
ENDSEC;
END-ISO-10303-21;
